ISO-10303-21;
HEADER;
FILE_DESCRIPTION (('STEP AP214'),
    '1' );
FILE_NAME ('Lampshade.step',
    '2026-10-07T18:46:32',
    ( '' ),
    ( '' ),
    'SwSTEP 2.0',
    'SolidWorks 2020',
    '' );
FILE_SCHEMA (( 'AUTOMOTIVE_DESIGN' ));
ENDSEC;

DATA;
#23=VECTOR ( 'NONE', #7523, 1000.000000000000000 ) ;
#47=FACE_OUTER_BOUND ( 'NONE', #3207, .T. ) ;
#53=EDGE_LOOP ( 'NONE', ( #6761, #19284, #17664, #12954 ) ) ;
#56=LINE ( 'NONE', #3411, #9523 ) ;
#60=CYLINDRICAL_SURFACE ( 'NONE', #9129, 0.2999999999999999334 ) ;
#69=AXIS2_PLACEMENT_3D ( 'NONE', #3279, #6875, #15230 ) ;
#73=FACE_OUTER_BOUND ( 'NONE', #20009, .T. ) ;
#92=DIRECTION ( 'NONE',  ( 0.000000000000000000, 0.000000000000000000, -1.000000000000000000 ) ) ;
#108=LINE ( 'NONE', #1550, #19368 ) ;
#123=ORIENTED_EDGE ( 'NONE', *, *, #13664, .F. ) ;
#131=DIRECTION ( 'NONE',  ( 0.000000000000000000, 0.000000000000000000, -1.000000000000000000 ) ) ;
#146=CARTESIAN_POINT ( 'NONE',  ( -33.50000000000001421, -84.70000000000001705, 78.20000000000000284 ) ) ;
#150=PLANE ( 'NONE',  #5314 ) ;
#177=CARTESIAN_POINT ( 'NONE',  ( 33.79999999999999005, 84.70000000000001705, 80.00000000000000000 ) ) ;
#180=CARTESIAN_POINT ( 'NONE',  ( -30.79999999999999361, -84.70000000000001705, 1.200000000000000400 ) ) ;
#181=DIRECTION ( 'NONE',  ( -1.788744114411106313E-17, -1.000000000000000000, -1.095289877103613968E-33 ) ) ;
#184=CARTESIAN_POINT ( 'NONE',  ( 33.19999999999999574, -84.70000000000001705, 78.20000000000000284 ) ) ;
#216=ORIENTED_EDGE ( 'NONE', *, *, #18835, .T. ) ;
#240=VECTOR ( 'NONE', #10804, 1000.000000000000000 ) ;
#248=EDGE_LOOP ( 'NONE', ( #16951, #8078, #4613, #17088 ) ) ;
#263=FILL_AREA_STYLE_COLOUR ( '', #16882 ) ;
#271=LINE ( 'NONE', #10799, #1678 ) ;
#306=ORIENTED_EDGE ( 'NONE', *, *, #13681, .T. ) ;
#313=ORIENTED_EDGE ( 'NONE', *, *, #15004, .T. ) ;
#317=DIRECTION ( 'NONE',  ( 0.000000000000000000, 0.000000000000000000, -1.000000000000000000 ) ) ;
#341=VERTEX_POINT ( 'NONE', #9025 ) ;
#353=CARTESIAN_POINT ( 'NONE',  ( -30.19999999999999574, 70.00000000000000000, -1.734723475976807094E-15 ) ) ;
#368=EDGE_LOOP ( 'NONE', ( #20999, #1461, #7336 ) ) ;
#369=CARTESIAN_POINT ( 'NONE',  ( -35.00000000000000000, 84.70000000000001705, 0.6000000000000033085 ) ) ;
#390=ORIENTED_EDGE ( 'NONE', *, *, #7630, .F. ) ;
#437=ORIENTED_EDGE ( 'NONE', *, *, #20643, .F. ) ;
#445=VERTEX_POINT ( 'NONE', #5264 ) ;
#452=ADVANCED_FACE ( 'NONE', ( #21117 ), #7672, .T. ) ;
#456=CARTESIAN_POINT ( 'NONE',  ( 34.39999999999998437, 84.70000000000001705, 79.70000000000000284 ) ) ;
#464=ORIENTED_EDGE ( 'NONE', *, *, #4413, .T. ) ;
#465=ORIENTED_EDGE ( 'NONE', *, *, #17617, .T. ) ;
#466=EDGE_CURVE ( 'NONE', #4617, #17770, #11667, .T. ) ;
#482=ORIENTED_EDGE ( 'NONE', *, *, #11769, .F. ) ;
#499=DIRECTION ( 'NONE',  ( -1.000000000000000000, 0.000000000000000000, 0.000000000000000000 ) ) ;
#509=AXIS2_PLACEMENT_3D ( 'NONE', #15002, #3029, #1454 ) ;
#535=VECTOR ( 'NONE', #9552, 1000.000000000000000 ) ;
#537=CARTESIAN_POINT ( 'NONE',  ( -30.19999999999999574, 69.70000000000001705, 1.199999999999999734 ) ) ;
#540=ORIENTED_EDGE ( 'NONE', *, *, #20299, .T. ) ;
#549=ORIENTED_EDGE ( 'NONE', *, *, #19963, .F. ) ;
#552=AXIS2_PLACEMENT_3D ( 'NONE', #2168, #5667, #18862 ) ;
#555=CARTESIAN_POINT ( 'NONE',  ( -1.836970198721042383E-17, 85.00000000000000000, 0.3000000000000021538 ) ) ;
#560=CARTESIAN_POINT ( 'NONE',  ( -33.20000000000000284, 84.70000000000001705, 1.800000000000000266 ) ) ;
#566=ORIENTED_EDGE ( 'NONE', *, *, #11700, .T. ) ;
#579=DIRECTION ( 'NONE',  ( 1.000000000000000000, -0.000000000000000000, 6.123233995736764803E-17 ) ) ;
#583=VERTEX_POINT ( 'NONE', #8007 ) ;
#595=EDGE_LOOP ( 'NONE', ( #11628, #11075, #18047, #10530 ) ) ;
#608=AXIS2_PLACEMENT_3D ( 'NONE', #14616, #16410, #8029 ) ;
#632=DIRECTION ( 'NONE',  ( -6.123233995736764803E-17, -0.000000000000000000, 1.000000000000000000 ) ) ;
#648=DIRECTION ( 'NONE',  ( 0.000000000000000000, 0.000000000000000000, -1.000000000000000000 ) ) ;
#652=VECTOR ( 'NONE', #1913, 1000.000000000000000 ) ;
#659=CIRCLE ( 'NONE', #15255, 0.5999999999999998668 ) ;
#662=DIRECTION ( 'NONE',  ( 1.000000000000000000, 0.000000000000000000, 0.000000000000000000 ) ) ;
#675=VERTEX_POINT ( 'NONE', #12002 ) ;
#697=CARTESIAN_POINT ( 'NONE',  ( 30.79999999999999716, -85.00000000000000000, 1.200000000000004174 ) ) ;
#713=DIRECTION ( 'NONE',  ( 1.788744114411106313E-17, 1.000000000000000000, 1.095289877103613968E-33 ) ) ;
#722=DIRECTION ( 'NONE',  ( 0.000000000000000000, 0.000000000000000000, -1.000000000000000000 ) ) ;
#731=EDGE_CURVE ( 'NONE', #3842, #12280, #19290, .T. ) ;
#733=EDGE_CURVE ( 'NONE', #13680, #14946, #8024, .T. ) ;
#740=DIRECTION ( 'NONE',  ( 0.000000000000000000, 0.000000000000000000, -1.000000000000000000 ) ) ;
#773=DIRECTION ( 'NONE',  ( 0.000000000000000000, 0.000000000000000000, 1.000000000000000000 ) ) ;
#783=ORIENTED_EDGE ( 'NONE', *, *, #6213, .F. ) ;
#789=CARTESIAN_POINT ( 'NONE',  ( 34.39999999999998437, 84.70000000000001705, 0.6000000000000041966 ) ) ;
#793=CIRCLE ( 'NONE', #21886, 0.2999999999999999334 ) ;
#794=DIRECTION ( 'NONE',  ( 0.000000000000000000, 1.000000000000000000, 0.000000000000000000 ) ) ;
#800=DIRECTION ( 'NONE',  ( 0.000000000000000000, 0.000000000000000000, -1.000000000000000000 ) ) ;
#810=LINE ( 'NONE', #4507, #7614 ) ;
#813=DIRECTION ( 'NONE',  ( 1.987703982890080681E-15, 0.000000000000000000, -1.000000000000000000 ) ) ;
#814=VERTEX_POINT ( 'NONE', #4241 ) ;
#815=DIRECTION ( 'NONE',  ( -8.673617379884034239E-17, -0.000000000000000000, 1.000000000000000000 ) ) ;
#823=VERTEX_POINT ( 'NONE', #13046 ) ;
#825=EDGE_CURVE ( 'NONE', #3127, #1963, #7517, .T. ) ;
#843=ORIENTED_EDGE ( 'NONE', *, *, #15926, .F. ) ;
#846=DIRECTION ( 'NONE',  ( -1.734723475976806848E-16, 0.000000000000000000, 1.000000000000000000 ) ) ;
#848=ORIENTED_EDGE ( 'NONE', *, *, #1937, .F. ) ;
#856=CARTESIAN_POINT ( 'NONE',  ( -33.20000000000000284, -84.70000000000001705, 1.500000000000000222 ) ) ;
#865=EDGE_CURVE ( 'NONE', #8082, #15018, #16059, .T. ) ;
#872=EDGE_LOOP ( 'NONE', ( #19202, #1679, #14033, #20667 ) ) ;
#873=AXIS2_PLACEMENT_3D ( 'NONE', #4273, #7741, #19821 ) ;
#876=EDGE_CURVE ( 'NONE', #7599, #21952, #14988, .T. ) ;
#882=DIRECTION ( 'NONE',  ( 0.000000000000000000, -0.000000000000000000, -1.000000000000000000 ) ) ;
#891=DIRECTION ( 'NONE',  ( -1.000000000000000000, 0.000000000000000000, 0.000000000000000000 ) ) ;
#896=AXIS2_PLACEMENT_3D ( 'NONE', #20030, #2782, #14749 ) ;
#899=PRESENTATION_STYLE_ASSIGNMENT (( #16222 ) ) ;
#904=CIRCLE ( 'NONE', #17692, 0.2999999999999999334 ) ;
#918=LINE ( 'NONE', #2387, #535 ) ;
#920=VECTOR ( 'NONE', #17928, 1000.000000000000000 ) ;
#924=LINE ( 'NONE', #19848, #3788 ) ;
#951=AXIS2_PLACEMENT_3D ( 'NONE', #6007, #19418, #12673 ) ;
#958=FACE_OUTER_BOUND ( 'NONE', #13559, .T. ) ;
#968=ORIENTED_EDGE ( 'NONE', *, *, #6974, .F. ) ;
#982=FACE_OUTER_BOUND ( 'NONE', #19148, .T. ) ;
#993=ORIENTED_EDGE ( 'NONE', *, *, #3228, .F. ) ;
#1013=ADVANCED_FACE ( 'NONE', ( #20460 ), #10015, .T. ) ;
#1041=CARTESIAN_POINT ( 'NONE',  ( 34.39999999999998437, -85.00000000000000000, 79.39999999999999147 ) ) ;
#1044=ORIENTED_EDGE ( 'NONE', *, *, #10066, .T. ) ;
#1046=LINE ( 'NONE', #18163, #21312 ) ;
#1065=ORIENTED_EDGE ( 'NONE', *, *, #7876, .T. ) ;
#1073=EDGE_CURVE ( 'NONE', #4505, #15052, #1868, .T. ) ;
#1083=CARTESIAN_POINT ( 'NONE',  ( 34.69999999999998863, 85.00000000000000000, 79.39999999999999147 ) ) ;
#1084=ORIENTED_EDGE ( 'NONE', *, *, #5957, .T. ) ;
#1085=ORIENTED_EDGE ( 'NONE', *, *, #1135, .F. ) ;
#1087=CIRCLE ( 'NONE', #16451, 0.5999999999999999778 ) ;
#1101=DIRECTION ( 'NONE',  ( 0.000000000000000000, -1.000000000000000000, 0.000000000000000000 ) ) ;
#1112=AXIS2_PLACEMENT_3D ( 'NONE', #16943, #12011, #18859 ) ;
#1135=EDGE_CURVE ( 'NONE', #7001, #7855, #19018, .T. ) ;
#1155=ORIENTED_EDGE ( 'NONE', *, *, #11973, .T. ) ;
#1160=CARTESIAN_POINT ( 'NONE',  ( -30.79999999999999361, -85.00000000000000000, 0.3000000000000002665 ) ) ;
#1166=DIRECTION ( 'NONE',  ( 0.000000000000000000, 0.000000000000000000, -1.000000000000000000 ) ) ;
#1167=DIRECTION ( 'NONE',  ( 0.000000000000000000, -1.000000000000000000, 0.000000000000000000 ) ) ;
#1172=DIRECTION ( 'NONE',  ( 0.000000000000000000, 0.000000000000000000, -1.000000000000000000 ) ) ;
#1189=DIRECTION ( 'NONE',  ( 0.000000000000000000, -1.000000000000000000, 0.000000000000000000 ) ) ;
#1190=DIRECTION ( 'NONE',  ( -1.000000000000000000, 0.000000000000000000, -8.673617379884034239E-17 ) ) ;
#1205=EDGE_CURVE ( 'NONE', #6175, #20684, #13282, .T. ) ;
#1219=FACE_OUTER_BOUND ( 'NONE', #9911, .T. ) ;
#1220=DIRECTION ( 'NONE',  ( 1.000000000000000000, 0.000000000000000000, 0.000000000000000000 ) ) ;
#1222=AXIS2_PLACEMENT_3D ( 'NONE', #14000, #17477, #12302 ) ;
#1228=PRODUCT ( 'Lampshade', 'Lampshade', '', ( #20396 ) ) ;
#1237=DIRECTION ( 'NONE',  ( 0.000000000000000000, 0.000000000000000000, 1.000000000000000000 ) ) ;
#1290=ORIENTED_EDGE ( 'NONE', *, *, #17720, .F. ) ;
#1298=EDGE_CURVE ( 'NONE', #11071, #583, #7567, .T. ) ;
#1305=DIRECTION ( 'NONE',  ( 0.000000000000000000, 0.000000000000000000, -1.000000000000000000 ) ) ;
#1316=EDGE_LOOP ( 'NONE', ( #8205, #5330, #1841, #11143 ) ) ;
#1321=CLOSED_SHELL ( 'NONE', ( #18011, #21293, #21672, #5432, #6026, #18113, #10541, #12822, #6337, #10935, #18987, #12640, #20548, #19431, #3631, #21052, #18522, #8958, #13304, #3118, #4749, #6859, #4343, #11185, #5214, #5607, #21919, #16779, #6308, #15466, #14203, #452, #5743, #8639, #8664, #10211, #10888, #14993, #4284, #14406, #19041, #19233, #10753, #8394, #13839, #1993, #12774, #10492, #12729, #5683, #17441, #8705, #17229, #21751, #17087, #2750, #8864, #8180, #13650, #9553, #19453, #4425, #17157, #4152, #7292, #1013, #13633, #2457, #20762, #2460, #16647, #1862, #3376 ) ) ;
#1336=CIRCLE ( 'NONE', #4208, 0.2999999999999947153 ) ;
#1338=CARTESIAN_POINT ( 'NONE',  ( -33.20000000000001705, -84.70000000000001705, 78.20000000000000284 ) ) ;
#1343=AXIS2_PLACEMENT_3D ( 'NONE', #14433, #13924, #8589 ) ;
#1353=( NAMED_UNIT ( * ) SI_UNIT ( $, .STERADIAN. ) SOLID_ANGLE_UNIT ( ) );
#1362=AXIS2_PLACEMENT_3D ( 'NONE', #3889, #499, #10709 ) ;
#1389=AXIS2_PLACEMENT_3D ( 'NONE', #8012, #11570, #22120 ) ;
#1424=AXIS2_PLACEMENT_3D ( 'NONE', #21915, #18540, #11812 ) ;
#1427=CARTESIAN_POINT ( 'NONE',  ( 33.19999999999999574, 84.70000000000001705, 78.20000000000000284 ) ) ;
#1428=PRODUCT_DEFINITION_SHAPE ( 'NONE', 'NONE',  #16121 ) ;
#1432=DIRECTION ( 'NONE',  ( 8.673617379884034239E-17, 0.000000000000000000, -1.000000000000000000 ) ) ;
#1452=FACE_OUTER_BOUND ( 'NONE', #11053, .T. ) ;
#1454=DIRECTION ( 'NONE',  ( 0.000000000000000000, 0.000000000000000000, -1.000000000000000000 ) ) ;
#1461=ORIENTED_EDGE ( 'NONE', *, *, #16756, .T. ) ;
#1474=CARTESIAN_POINT ( 'NONE',  ( -35.00000000000000000, 70.29999999999999716, 0.000000000000000000 ) ) ;
#1487=ORIENTED_EDGE ( 'NONE', *, *, #14223, .F. ) ;
#1489=CARTESIAN_POINT ( 'NONE',  ( 30.19999999999999574, 69.70000000000000284, 0.3000000000000033751 ) ) ;
#1491=EDGE_CURVE ( 'NONE', #9271, #2915, #21371, .T. ) ;
#1507=LINE ( 'NONE', #21998, #12637 ) ;
#1530=DIRECTION ( 'NONE',  ( -0.000000000000000000, -0.000000000000000000, -1.000000000000000000 ) ) ;
#1550=CARTESIAN_POINT ( 'NONE',  ( 0.000000000000000000, -85.00000000000000000, 78.79999999999999716 ) ) ;
#1553=EDGE_CURVE ( 'NONE', #20330, #9891, #8489, .T. ) ;
#1567=VECTOR ( 'NONE', #2688, 1000.000000000000000 ) ;
#1578=EDGE_LOOP ( 'NONE', ( #13780, #306, #5689, #3602 ) ) ;
#1580=EDGE_CURVE ( 'NONE', #9271, #21431, #2754, .T. ) ;
#1594=EDGE_CURVE ( 'NONE', #2890, #7001, #6711, .T. ) ;
#1607=CARTESIAN_POINT ( 'NONE',  ( 34.39999999999998437, -84.70000000000001705, 0.6000000000000041966 ) ) ;
#1629=EDGE_LOOP ( 'NONE', ( #15851, #6021, #13552, #4373 ) ) ;
#1634=ORIENTED_EDGE ( 'NONE', *, *, #15888, .F. ) ;
#1663=ORIENTED_EDGE ( 'NONE', *, *, #11252, .T. ) ;
#1665=CIRCLE ( 'NONE', #6335, 0.3000000000000016542 ) ;
#1666=DIRECTION ( 'NONE',  ( 1.000000000000000000, 0.000000000000000000, 0.000000000000000000 ) ) ;
#1678=VECTOR ( 'NONE', #12334, 1000.000000000000000 ) ;
#1679=ORIENTED_EDGE ( 'NONE', *, *, #9739, .F. ) ;
#1685=ORIENTED_EDGE ( 'NONE', *, *, #21805, .T. ) ;
#1703=CIRCLE ( 'NONE', #8854, 0.6000000000000033085 ) ;
#1730=CARTESIAN_POINT ( 'NONE',  ( 30.49999999999999645, -84.70000000000001705, 1.500000000000004885 ) ) ;
#1751=DIRECTION ( 'NONE',  ( -1.000000000000000000, 0.000000000000000000, -6.123233995736764803E-17 ) ) ;
#1752=CARTESIAN_POINT ( 'NONE',  ( 30.79999999999999716, -84.70000000000001705, 0.3000000000000039857 ) ) ;
#1771=CARTESIAN_POINT ( 'NONE',  ( 33.49999999999998579, 85.00000000000000000, 80.00000000000000000 ) ) ;
#1775=LINE ( 'NONE', #6943, #18074 ) ;
#1780=VERTEX_POINT ( 'NONE', #15940 ) ;
#1782=EDGE_CURVE ( 'NONE', #10170, #6971, #21129, .T. ) ;
#1792=CARTESIAN_POINT ( 'NONE',  ( 34.99999999999999289, 84.70000000000001705, 79.39999999999999147 ) ) ;
#1805=ORIENTED_EDGE ( 'NONE', *, *, #1553, .T. ) ;
#1816=DIRECTION ( 'NONE',  ( 0.000000000000000000, -1.000000000000000000, 0.000000000000000000 ) ) ;
#1841=ORIENTED_EDGE ( 'NONE', *, *, #4561, .F. ) ;
#1848=DIRECTION ( 'NONE',  ( 0.000000000000000000, 0.000000000000000000, -1.000000000000000000 ) ) ;
#1854=EDGE_LOOP ( 'NONE', ( #3811, #6917, #21170, #465 ) ) ;
#1859=DIRECTION ( 'NONE',  ( -1.000000000000000000, 0.000000000000000000, 0.000000000000000000 ) ) ;
#1862=ADVANCED_FACE ( 'NONE', ( #14715 ), #6235, .T. ) ;
#1868=LINE ( 'NONE', #17626, #2570 ) ;
#1877=EDGE_LOOP ( 'NONE', ( #1805, #12815, #11451, #7475 ) ) ;
#1879=DIRECTION ( 'NONE',  ( 0.000000000000000000, -1.000000000000000000, 0.000000000000000000 ) ) ;
#1901=ORIENTED_EDGE ( 'NONE', *, *, #1594, .F. ) ;
#1913=DIRECTION ( 'NONE',  ( 8.673617379884034239E-17, 0.000000000000000000, -1.000000000000000000 ) ) ;
#1914=CARTESIAN_POINT ( 'NONE',  ( -34.70000000000000284, 85.00000000000000000, -6.019490461639519829E-15 ) ) ;
#1928=ORIENTED_EDGE ( 'NONE', *, *, #19642, .T. ) ;
#1937=EDGE_CURVE ( 'NONE', #12578, #16703, #1507, .T. ) ;
#1958=DIRECTION ( 'NONE',  ( -0.000000000000000000, 1.000000000000000000, -0.000000000000000000 ) ) ;
#1963=VERTEX_POINT ( 'NONE', #18397 ) ;
#1970=ORIENTED_EDGE ( 'NONE', *, *, #15249, .F. ) ;
#1972=EDGE_CURVE ( 'NONE', #20684, #19413, #13364, .T. ) ;
#1973=ORIENTED_EDGE ( 'NONE', *, *, #1553, .F. ) ;
#1975=VERTEX_POINT ( 'NONE', #4768 ) ;
#1993=ADVANCED_FACE ( 'NONE', ( #16726 ), #15143, .T. ) ;
#2003=DIRECTION ( 'NONE',  ( -1.000000000000000000, 0.000000000000000000, 0.000000000000000000 ) ) ;
#2006=TOROIDAL_SURFACE ( 'NONE', #14504, 0.5999999999999999778, 0.2999999999999999889 ) ;
#2012=ORIENTED_EDGE ( 'NONE', *, *, #14108, .T. ) ;
#2028=LINE ( 'NONE', #10979, #17923 ) ;
#2033=ORIENTED_EDGE ( 'NONE', *, *, #19476, .T. ) ;
#2036=LINE ( 'NONE', #10549, #9246 ) ;
#2037=ORIENTED_EDGE ( 'NONE', *, *, #21928, .F. ) ;
#2038=AXIS2_PLACEMENT_3D ( 'NONE', #8317, #1816, #8653 ) ;
#2040=CIRCLE ( 'NONE', #14538, 0.3000000000000016542 ) ;
#2068=CARTESIAN_POINT ( 'NONE',  ( 33.49999999999998579, 84.70000000000001705, 78.50000000000000000 ) ) ;
#2083=AXIS2_PLACEMENT_3D ( 'NONE', #12956, #9289, #773 ) ;
#2102=CIRCLE ( 'NONE', #16762, 0.5999999999999999778 ) ;
#2128=AXIS2_PLACEMENT_3D ( 'NONE', #21365, #11161, #16291 ) ;
#2132=ORIENTED_EDGE ( 'NONE', *, *, #12800, .F. ) ;
#2137=LINE ( 'NONE', #555, #7712 ) ;
#2149=CARTESIAN_POINT ( 'NONE',  ( 30.79999999999999716, 69.70000000000000284, 4.029087969194791265E-15 ) ) ;
#2168=CARTESIAN_POINT ( 'NONE',  ( -33.50000000000001421, 85.00000000000000000, 80.00000000000000000 ) ) ;
#2185=DIRECTION ( 'NONE',  ( 0.000000000000000000, 0.000000000000000000, -1.000000000000000000 ) ) ;
#2191=ORIENTED_EDGE ( 'NONE', *, *, #21928, .T. ) ;
#2194=CYLINDRICAL_SURFACE ( 'NONE', #1362, 0.2999999999999947153 ) ;
#2206=ORIENTED_EDGE ( 'NONE', *, *, #8421, .T. ) ;
#2214=CARTESIAN_POINT ( 'NONE',  ( -33.80000000000000426, -85.00000000000000000, 1.800000000000000266 ) ) ;
#2217=AXIS2_PLACEMENT_3D ( 'NONE', #5414, #5638, #10540 ) ;
#2245=DIRECTION ( 'NONE',  ( 0.000000000000000000, 0.000000000000000000, -1.000000000000000000 ) ) ;
#2246=DIRECTION ( 'NONE',  ( -6.123233995736764803E-17, 0.000000000000000000, 1.000000000000000000 ) ) ;
#2309=DIRECTION ( 'NONE',  ( 1.000000000000000000, 0.000000000000000000, 6.123233995736764803E-17 ) ) ;
#2322=CIRCLE ( 'NONE', #14820, 0.5999999999999998668 ) ;
#2332=AXIS2_PLACEMENT_3D ( 'NONE', #8185, #11519, #5151 ) ;
#2334=CARTESIAN_POINT ( 'NONE',  ( 34.69999999999998863, -85.00000000000000000, 79.39999999999999147 ) ) ;
#2337=CIRCLE ( 'NONE', #10916, 0.2999999999999947153 ) ;
#2356=DIRECTION ( 'NONE',  ( 0.000000000000000000, -1.000000000000000000, 0.000000000000000000 ) ) ;
#2376=AXIS2_PLACEMENT_3D ( 'NONE', #184, #1879, #20803 ) ;
#2382=CARTESIAN_POINT ( 'NONE',  ( -35.00000000000000000, -84.70000000000001705, 1.500000000000000000 ) ) ;
#2387=CARTESIAN_POINT ( 'NONE',  ( -33.50000000000001421, 84.70000000000001705, 78.50000000000000000 ) ) ;
#2414=AXIS2_PLACEMENT_3D ( 'NONE', #21482, #1189, #13279 ) ;
#2447=CARTESIAN_POINT ( 'NONE',  ( 34.39999999999998437, 85.00000000000000000, 79.39999999999999147 ) ) ;
#2454=AXIS2_PLACEMENT_3D ( 'NONE', #12944, #9615, #21488 ) ;
#2457=ADVANCED_FACE ( 'NONE', ( #14649 ), #11409, .T. ) ;
#2460=ADVANCED_FACE ( 'NONE', ( #12961 ), #19023, .T. ) ;
#2465=ORIENTED_EDGE ( 'NONE', *, *, #11344, .F. ) ;
#2468=AXIS2_PLACEMENT_3D ( 'NONE', #13944, #20689, #20795 ) ;
#2470=DIRECTION ( 'NONE',  ( 0.000000000000000000, -1.000000000000000000, 0.000000000000000000 ) ) ;
#2475=DIRECTION ( 'NONE',  ( 0.000000000000000000, -1.000000000000000000, 0.000000000000000000 ) ) ;
#2479=CARTESIAN_POINT ( 'NONE',  ( -33.80000000000001847, 84.70000000000001705, 80.00000000000000000 ) ) ;
#2497=LINE ( 'NONE', #2382, #20041 ) ;
#2505=DIRECTION ( 'NONE',  ( -0.000000000000000000, 1.000000000000000000, -0.000000000000000000 ) ) ;
#2532=EDGE_LOOP ( 'NONE', ( #11726, #11430, #19783, #12810 ) ) ;
#2550=EDGE_CURVE ( 'NONE', #10124, #21689, #56, .T. ) ;
#2570=VECTOR ( 'NONE', #21005, 1000.000000000000000 ) ;
#2596=FACE_OUTER_BOUND ( 'NONE', #20416, .T. ) ;
#2604=DIRECTION ( 'NONE',  ( -1.000000000000000000, 0.000000000000000000, -6.123233995736764803E-17 ) ) ;
#2635=DIRECTION ( 'NONE',  ( 1.000000000000000000, 0.000000000000000000, 1.734723475976786140E-16 ) ) ;
#2657=DIRECTION ( 'NONE',  ( 0.000000000000000000, 0.000000000000000000, -1.000000000000000000 ) ) ;
#2661=DIRECTION ( 'NONE',  ( 1.788744114411106313E-17, 1.000000000000000000, 1.095289877103613968E-33 ) ) ;
#2665=CYLINDRICAL_SURFACE ( 'NONE', #4266, 0.5999999999999999778 ) ;
#2688=DIRECTION ( 'NONE',  ( -1.000000000000000000, 0.000000000000000000, -6.123233995736764803E-17 ) ) ;
#2700=EDGE_LOOP ( 'NONE', ( #15288, #10930, #20717, #4285 ) ) ;
#2710=CARTESIAN_POINT ( 'NONE',  ( 30.49999999999999645, -123.9599366953518711, 0.3000000000000033751 ) ) ;
#2750=ADVANCED_FACE ( 'NONE', ( #16132 ), #6507, .T. ) ;
#2754=CIRCLE ( 'NONE', #15254, 0.2999999999999947153 ) ;
#2782=DIRECTION ( 'NONE',  ( 1.734723475976806848E-16, 0.000000000000000000, -1.000000000000000000 ) ) ;
#2796=ORIENTED_EDGE ( 'NONE', *, *, #21723, .F. ) ;
#2807=FACE_OUTER_BOUND ( 'NONE', #1578, .T. ) ;
#2832=ORIENTED_EDGE ( 'NONE', *, *, #21476, .F. ) ;
#2836=ORIENTED_EDGE ( 'NONE', *, *, #13992, .F. ) ;
#2846=DIRECTION ( 'NONE',  ( -1.000000000000000000, 0.000000000000000000, -1.987703982890080681E-15 ) ) ;
#2849=ORIENTED_EDGE ( 'NONE', *, *, #21144, .F. ) ;
#2860=ORIENTED_EDGE ( 'NONE', *, *, #5270, .F. ) ;
#2863=CARTESIAN_POINT ( 'NONE',  ( 30.79999999999999716, -85.00000000000000000, 0.3000000000000039857 ) ) ;
#2868=CARTESIAN_POINT ( 'NONE',  ( 30.79999999999999716, -123.9599366953518711, 1.200000000000003064 ) ) ;
#2874=ORIENTED_EDGE ( 'NONE', *, *, #8795, .F. ) ;
#2878=CIRCLE ( 'NONE', #15731, 0.2999999999999947153 ) ;
#2885=EDGE_LOOP ( 'NONE', ( #566, #4696, #15517, #3939 ) ) ;
#2890=VERTEX_POINT ( 'NONE', #18271 ) ;
#2893=AXIS2_PLACEMENT_3D ( 'NONE', #16101, #7628, #6068 ) ;
#2901=EDGE_CURVE ( 'NONE', #1780, #20330, #810, .T. ) ;
#2915=VERTEX_POINT ( 'NONE', #15125 ) ;
#2918=EDGE_CURVE ( 'NONE', #20326, #5502, #17145, .T. ) ;
#2932=VECTOR ( 'NONE', #13852, 1000.000000000000000 ) ;
#2933=CARTESIAN_POINT ( 'NONE',  ( -35.00000000000000000, -84.70000000000001705, 0.2999999999999999889 ) ) ;
#2940=EDGE_LOOP ( 'NONE', ( #8384, #1084, #8140, #19016 ) ) ;
#2969=CARTESIAN_POINT ( 'NONE',  ( -30.79999999999999005, 69.70000000000001705, 1.200000000000000400 ) ) ;
#2979=DIRECTION ( 'NONE',  ( 0.000000000000000000, 0.000000000000000000, -1.000000000000000000 ) ) ;
#3029=DIRECTION ( 'NONE',  ( -1.000000000000000000, -0.000000000000000000, 0.000000000000000000 ) ) ;
#3057=VERTEX_POINT ( 'NONE', #8872 ) ;
#3110=CARTESIAN_POINT ( 'NONE',  ( -7.347880794884131322E-17, -85.00000000000000000, 1.200000000000002176 ) ) ;
#3114=DIRECTION ( 'NONE',  ( 6.123233995736764803E-17, 0.000000000000000000, -1.000000000000000000 ) ) ;
#3118=ADVANCED_FACE ( 'NONE', ( #1219 ), #11418, .T. ) ;
#3121=CARTESIAN_POINT ( 'NONE',  ( 34.39999999999998437, 85.00000000000000000, 79.70000000000000284 ) ) ;
#3127=VERTEX_POINT ( 'NONE', #6412 ) ;
#3134=DIRECTION ( 'NONE',  ( 6.123233995736764803E-17, -0.000000000000000000, -1.000000000000000000 ) ) ;
#3153=DIRECTION ( 'NONE',  ( 0.000000000000000000, 0.000000000000000000, -1.000000000000000000 ) ) ;
#3156=VERTEX_POINT ( 'NONE', #18246 ) ;
#3162=ORIENTED_EDGE ( 'NONE', *, *, #17189, .T. ) ;
#3183=CYLINDRICAL_SURFACE ( 'NONE', #13133, 0.2999999999999999334 ) ;
#3193=ORIENTED_EDGE ( 'NONE', *, *, #6213, .T. ) ;
#3195=SPHERICAL_SURFACE ( 'NONE', #1389, 0.2999999999999999889 ) ;
#3197=AXIS2_PLACEMENT_3D ( 'NONE', #5832, #19915, #16301 ) ;
#3207=EDGE_LOOP ( 'NONE', ( #4363, #17940, #19767, #1155, #18757, #12244, #12082, #549, #5858, #8352, #313, #16200, #9657, #16273, #12947, #19912, #16431, #11487, #5818, #4853 ) ) ;
#3212=AXIS2_PLACEMENT_3D ( 'NONE', #4568, #6045, #9382 ) ;
#3228=EDGE_CURVE ( 'NONE', #1963, #341, #18014, .T. ) ;
#3235=EDGE_CURVE ( 'NONE', #4063, #445, #10511, .T. ) ;
#3248=ORIENTED_EDGE ( 'NONE', *, *, #20859, .T. ) ;
#3264=LINE ( 'NONE', #17012, #3537 ) ;
#3277=CYLINDRICAL_SURFACE ( 'NONE', #2038, 0.6000000000000033085 ) ;
#3279=CARTESIAN_POINT ( 'NONE',  ( 34.39999999999998437, -85.00000000000000000, 0.6000000000000041966 ) ) ;
#3282=DIRECTION ( 'NONE',  ( 0.000000000000000000, 0.000000000000000000, -1.000000000000000000 ) ) ;
#3285=CIRCLE ( 'NONE', #13289, 0.2999999999999999889 ) ;
#3322=FACE_OUTER_BOUND ( 'NONE', #20839, .T. ) ;
#3328=DIRECTION ( 'NONE',  ( -1.000000000000000000, -0.000000000000000000, 0.000000000000000000 ) ) ;
#3333=CYLINDRICAL_SURFACE ( 'NONE', #15912, 0.3000000000000016542 ) ;
#3345=ORIENTED_EDGE ( 'NONE', *, *, #11344, .T. ) ;
#3347=EDGE_CURVE ( 'NONE', #2915, #675, #7303, .T. ) ;
#3376=ADVANCED_FACE ( 'NONE', ( #1452 ), #5520, .T. ) ;
#3378=ORIENTED_EDGE ( 'NONE', *, *, #10066, .F. ) ;
#3394=CARTESIAN_POINT ( 'NONE',  ( -33.80000000000000426, 85.00000000000000000, 1.500000000000001332 ) ) ;
#3411=CARTESIAN_POINT ( 'NONE',  ( -33.50000000000001421, -85.00000000000000000, 78.20000000000000284 ) ) ;
#3424=EDGE_LOOP ( 'NONE', ( #10140, #16440, #9658, #1663 ) ) ;
#3426=CYLINDRICAL_SURFACE ( 'NONE', #21092, 0.3000000000000016542 ) ;
#3431=CARTESIAN_POINT ( 'NONE',  ( -34.40000000000001279, -85.00000000000000000, 79.70000000000000284 ) ) ;
#3434=CIRCLE ( 'NONE', #9131, 0.2999999999999999334 ) ;
#3439=CARTESIAN_POINT ( 'NONE',  ( -34.39999999999999858, -84.70000000000001705, 0.3000000000000033196 ) ) ;
#3445=ORIENTED_EDGE ( 'NONE', *, *, #18026, .T. ) ;
#3448=CARTESIAN_POINT ( 'NONE',  ( 30.19999999999999574, 70.00000000000000000, 1.500000000000004885 ) ) ;
#3457=ORIENTED_EDGE ( 'NONE', *, *, #13316, .F. ) ;
#3473=CARTESIAN_POINT ( 'NONE',  ( -30.79999999999999005, 69.70000000000001705, 0.2999999999999999334 ) ) ;
#3486=VERTEX_POINT ( 'NONE', #13969 ) ;
#3532=VECTOR ( 'NONE', #21595, 1000.000000000000000 ) ;
#3537=VECTOR ( 'NONE', #20272, 1000.000000000000000 ) ;
#3551=DIRECTION ( 'NONE',  ( 0.000000000000000000, 0.000000000000000000, -1.000000000000000000 ) ) ;
#3561=EDGE_CURVE ( 'NONE', #3486, #14859, #9988, .T. ) ;
#3577=ORIENTED_EDGE ( 'NONE', *, *, #4685, .T. ) ;
#3583=ORIENTED_EDGE ( 'NONE', *, *, #21569, .F. ) ;
#3602=ORIENTED_EDGE ( 'NONE', *, *, #3561, .T. ) ;
#3605=EDGE_LOOP ( 'NONE', ( #8555, #15272, #13455, #14938 ) ) ;
#3610=AXIS2_PLACEMENT_3D ( 'NONE', #14941, #11475, #1172 ) ;
#3613=CIRCLE ( 'NONE', #5039, 0.6000000000000033085 ) ;
#3631=ADVANCED_FACE ( 'NONE', ( #4128 ), #2665, .T. ) ;
#3665=LINE ( 'NONE', #13503, #13123 ) ;
#3679=DIRECTION ( 'NONE',  ( -1.000000000000000000, 0.000000000000000000, 0.000000000000000000 ) ) ;
#3690=CARTESIAN_POINT ( 'NONE',  ( 34.39999999999998437, -85.00000000000000000, 0.3000000000000042077 ) ) ;
#3694=CARTESIAN_POINT ( 'NONE',  ( 34.39999999999998437, 85.00000000000000000, 0.3000000000000042077 ) ) ;
#3701=EDGE_CURVE ( 'NONE', #9271, #3754, #21051, .T. ) ;
#3716=CARTESIAN_POINT ( 'NONE',  ( 33.79999999999999716, -85.00000000000000000, 2.931682674400803201E-15 ) ) ;
#3721=PRODUCT_DEFINITION_FORMATION_WITH_SPECIFIED_SOURCE ( 'ANY', '', #1228, .NOT_KNOWN. ) ;
#3736=DIRECTION ( 'NONE',  ( 0.000000000000000000, 0.000000000000000000, -1.000000000000000000 ) ) ;
#3754=VERTEX_POINT ( 'NONE', #7845 ) ;
#3778=CARTESIAN_POINT ( 'NONE',  ( 34.69999999999998863, -84.70000000000001705, 79.39999999999999147 ) ) ;
#3788=VECTOR ( 'NONE', #11219, 1000.000000000000000 ) ;
#3794=EDGE_LOOP ( 'NONE', ( #9587, #437, #16232, #20032 ) ) ;
#3797=AXIS2_PLACEMENT_3D ( 'NONE', #20694, #3679, #15516 ) ;
#3803=PRODUCT_DEFINITION_CONTEXT ( 'detailed design', #12566, 'design' ) ;
#3809=LINE ( 'NONE', #2334, #4737 ) ;
#3811=ORIENTED_EDGE ( 'NONE', *, *, #3915, .T. ) ;
#3833=CIRCLE ( 'NONE', #5631, 0.5999999999999998668 ) ;
#3842=VERTEX_POINT ( 'NONE', #3121 ) ;
#3849=CIRCLE ( 'NONE', #7429, 0.2999999999999999889 ) ;
#3852=VECTOR ( 'NONE', #20774, 1000.000000000000000 ) ;
#3856=CARTESIAN_POINT ( 'NONE',  ( 34.99999999999999289, 85.00000000000000000, 0.6000000000000033085 ) ) ;
#3862=CARTESIAN_POINT ( 'NONE',  ( -33.20000000000000284, 85.00000000000000000, 1.800000000000000266 ) ) ;
#3864=AXIS2_PLACEMENT_3D ( 'NONE', #7246, #19205, #7139 ) ;
#3883=DIRECTION ( 'NONE',  ( 0.000000000000000000, -0.000000000000000000, -1.000000000000000000 ) ) ;
#3889=CARTESIAN_POINT ( 'NONE',  ( -35.00000000000001421, 84.70000000000001705, 78.79999999999999716 ) ) ;
#3896=DIRECTION ( 'NONE',  ( -1.000000000000000000, -0.000000000000000000, -0.000000000000000000 ) ) ;
#3915=EDGE_CURVE ( 'NONE', #823, #17660, #11942, .T. ) ;
#3932=LINE ( 'NONE', #7619, #4564 ) ;
#3939=ORIENTED_EDGE ( 'NONE', *, *, #7876, .F. ) ;
#3947=FACE_OUTER_BOUND ( 'NONE', #1316, .T. ) ;
#3948=DIRECTION ( 'NONE',  ( 0.000000000000000000, -1.000000000000000000, 0.000000000000000000 ) ) ;
#3960=( LENGTH_UNIT ( ) NAMED_UNIT ( * ) SI_UNIT ( .MILLI., .METRE. ) );
#3969=DIRECTION ( 'NONE',  ( 0.000000000000000000, 0.000000000000000000, -1.000000000000000000 ) ) ;
#3976=CYLINDRICAL_SURFACE ( 'NONE', #21521, 0.3000000000000001554 ) ;
#4022=AXIS2_PLACEMENT_3D ( 'NONE', #560, #8873, #15786 ) ;
#4050=CARTESIAN_POINT ( 'NONE',  ( 34.39999999999998437, 84.70000000000001705, 79.39999999999999147 ) ) ;
#4063=VERTEX_POINT ( 'NONE', #4337 ) ;
#4082=LINE ( 'NONE', #2068, #240 ) ;
#4086=VECTOR ( 'NONE', #5454, 1000.000000000000000 ) ;
#4097=LINE ( 'NONE', #6016, #18073 ) ;
#4122=FACE_OUTER_BOUND ( 'NONE', #8279, .T. ) ;
#4128=FACE_OUTER_BOUND ( 'NONE', #5758, .T. ) ;
#4152=ADVANCED_FACE ( 'NONE', ( #8467 ), #22139, .T. ) ;
#4167=EDGE_CURVE ( 'NONE', #15663, #7855, #1703, .T. ) ;
#4190=VECTOR ( 'NONE', #11614, 1000.000000000000000 ) ;
#4198=DIRECTION ( 'NONE',  ( -1.000000000000000000, 0.000000000000000000, -0.000000000000000000 ) ) ;
#4208=AXIS2_PLACEMENT_3D ( 'NONE', #18334, #9499, #4464 ) ;
#4224=CYLINDRICAL_SURFACE ( 'NONE', #6992, 0.2999999999999999889 ) ;
#4238=CIRCLE ( 'NONE', #18891, 0.2999999999999947153 ) ;
#4241=CARTESIAN_POINT ( 'NONE',  ( 34.99999999999999289, -84.70000000000001705, 79.39999999999999147 ) ) ;
#4266=AXIS2_PLACEMENT_3D ( 'NONE', #19797, #1101, #19568 ) ;
#4273=CARTESIAN_POINT ( 'NONE',  ( -33.20000000000001705, 85.00000000000000000, 78.20000000000000284 ) ) ;
#4284=ADVANCED_FACE ( 'NONE', ( #73 ), #8794, .T. ) ;
#4285=ORIENTED_EDGE ( 'NONE', *, *, #15925, .T. ) ;
#4305=DIRECTION ( 'NONE',  ( 0.000000000000000000, 0.000000000000000000, -1.000000000000000000 ) ) ;
#4312=CARTESIAN_POINT ( 'NONE',  ( -35.00000000000001421, 85.00000000000000000, 80.00000000000000000 ) ) ;
#4320=DIRECTION ( 'NONE',  ( -0.000000000000000000, 1.000000000000000000, 0.000000000000000000 ) ) ;
#4327=CARTESIAN_POINT ( 'NONE',  ( 30.19999999999999574, 70.29999999999999716, 1.200000000000003952 ) ) ;
#4329=DIRECTION ( 'NONE',  ( 6.123233995736764803E-17, -0.000000000000000000, -1.000000000000000000 ) ) ;
#4331=EDGE_LOOP ( 'NONE', ( #16767, #7747, #1634, #11147 ) ) ;
#4332=DIRECTION ( 'NONE',  ( 0.000000000000000000, -1.000000000000000000, 0.000000000000000000 ) ) ;
#4337=CARTESIAN_POINT ( 'NONE',  ( -34.39999999999999858, 85.00000000000000000, 0.3000000000000000444 ) ) ;
#4343=ADVANCED_FACE ( 'NONE', ( #11530 ), #16673, .T. ) ;
#4344=CIRCLE ( 'NONE', #1424, 0.2999999999999947153 ) ;
#4355=CARTESIAN_POINT ( 'NONE',  ( -30.49999999999999289, -84.70000000000001705, -1.716353773989596664E-15 ) ) ;
#4357=CYLINDRICAL_SURFACE ( 'NONE', #896, 0.3000000000000016542 ) ;
#4363=ORIENTED_EDGE ( 'NONE', *, *, #21144, .T. ) ;
#4373=ORIENTED_EDGE ( 'NONE', *, *, #19179, .T. ) ;
#4382=CYLINDRICAL_SURFACE ( 'NONE', #873, 0.2999999999999947153 ) ;
#4406=ORIENTED_EDGE ( 'NONE', *, *, #21806, .F. ) ;
#4407=ORIENTED_EDGE ( 'NONE', *, *, #17189, .F. ) ;
#4413=EDGE_CURVE ( 'NONE', #17830, #6609, #9209, .T. ) ;
#4419=CARTESIAN_POINT ( 'NONE',  ( 33.19999999999999574, 84.70000000000001705, 1.799999999999996048 ) ) ;
#4425=ADVANCED_FACE ( 'NONE', ( #2596 ), #15010, .T. ) ;
#4430=ORIENTED_EDGE ( 'NONE', *, *, #10623, .T. ) ;
#4456=FACE_OUTER_BOUND ( 'NONE', #4491, .T. ) ;
#4464=DIRECTION ( 'NONE',  ( 0.000000000000000000, 0.000000000000000000, 1.000000000000000000 ) ) ;
#4468=CARTESIAN_POINT ( 'NONE',  ( 33.79999999999999005, -85.00000000000000000, 78.20000000000000284 ) ) ;
#4485=CARTESIAN_POINT ( 'NONE',  ( -30.49999999999999289, -84.70000000000001705, 1.199999999999999734 ) ) ;
#4491=EDGE_LOOP ( 'NONE', ( #11357, #12934, #9710, #16876 ) ) ;
#4493=CIRCLE ( 'NONE', #21664, 0.2999999999999999334 ) ;
#4501=AXIS2_PLACEMENT_3D ( 'NONE', #19938, #9641, #18241 ) ;
#4505=VERTEX_POINT ( 'NONE', #15339 ) ;
#4507=CARTESIAN_POINT ( 'NONE',  ( -35.00000000000001421, 84.70000000000001705, 80.00000000000000000 ) ) ;
#4513=LINE ( 'NONE', #19629, #9853 ) ;
#4528=EDGE_CURVE ( 'NONE', #11049, #6609, #4238, .T. ) ;
#4539=DIRECTION ( 'NONE',  ( -0.000000000000000000, 1.000000000000000000, -0.000000000000000000 ) ) ;
#4561=EDGE_CURVE ( 'NONE', #4617, #2915, #19598, .T. ) ;
#4564=VECTOR ( 'NONE', #15977, 1000.000000000000000 ) ;
#4568=CARTESIAN_POINT ( 'NONE',  ( 30.79999999999999716, 69.70000000000000284, 0.3000000000000039857 ) ) ;
#4586=ORIENTED_EDGE ( 'NONE', *, *, #10757, .F. ) ;
#4597=AXIS2_PLACEMENT_3D ( 'NONE', #17053, #20534, #6901 ) ;
#4605=CIRCLE ( 'NONE', #19596, 0.2999999999999999334 ) ;
#4613=ORIENTED_EDGE ( 'NONE', *, *, #10091, .T. ) ;
#4617=VERTEX_POINT ( 'NONE', #18654 ) ;
#4641=EDGE_LOOP ( 'NONE', ( #3577, #10756, #2132 ) ) ;
#4643=CARTESIAN_POINT ( 'NONE',  ( -30.19999999999999574, 69.70000000000001705, 0.2999999999999999334 ) ) ;
#4644=DIRECTION ( 'NONE',  ( -0.000000000000000000, 1.000000000000000000, -0.000000000000000000 ) ) ;
#4672=ORIENTED_EDGE ( 'NONE', *, *, #12542, .F. ) ;
#4685=EDGE_CURVE ( 'NONE', #14491, #18912, #6745, .T. ) ;
#4692=VERTEX_POINT ( 'NONE', #6701 ) ;
#4696=ORIENTED_EDGE ( 'NONE', *, *, #2918, .F. ) ;
#4698=VECTOR ( 'NONE', #3328, 1000.000000000000000 ) ;
#4719=AXIS2_PLACEMENT_3D ( 'NONE', #7249, #20563, #5240 ) ;
#4737=VECTOR ( 'NONE', #7281, 1000.000000000000000 ) ;
#4741=EDGE_LOOP ( 'NONE', ( #15216, #13158, #10326, #22068 ) ) ;
#4749=ADVANCED_FACE ( 'NONE', ( #21001 ), #2194, .T. ) ;
#4768=CARTESIAN_POINT ( 'NONE',  ( -34.70000000000000284, -85.00000000000000000, 0.6000000000000033085 ) ) ;
#4779=CARTESIAN_POINT ( 'NONE',  ( -33.80000000000001847, 84.70000000000001705, 78.20000000000000284 ) ) ;
#4810=DIRECTION ( 'NONE',  ( 0.000000000000000000, 0.000000000000000000, -1.000000000000000000 ) ) ;
#4852=VECTOR ( 'NONE', #19993, 1000.000000000000000 ) ;
#4853=ORIENTED_EDGE ( 'NONE', *, *, #13334, .T. ) ;
#4854=DIRECTION ( 'NONE',  ( -1.000000000000000000, 0.000000000000000000, -6.123233995736764803E-17 ) ) ;
#4882=DIRECTION ( 'NONE',  ( 0.000000000000000000, 0.000000000000000000, 1.000000000000000000 ) ) ;
#4888=DIRECTION ( 'NONE',  ( -6.123233995736764803E-17, 0.000000000000000000, 1.000000000000000000 ) ) ;
#4900=AXIS2_PLACEMENT_3D ( 'NONE', #21616, #18568, #13075 ) ;
#4916=CIRCLE ( 'NONE', #11682, 0.6000000000000033085 ) ;
#4922=AXIS2_PLACEMENT_3D ( 'NONE', #16379, #4305, #14462 ) ;
#4923=AXIS2_PLACEMENT_3D ( 'NONE', #7975, #19825, #8200 ) ;
#4937=CARTESIAN_POINT ( 'NONE',  ( 33.49999999999998579, 84.70000000000001705, 78.20000000000000284 ) ) ;
#4944=EDGE_CURVE ( 'NONE', #21163, #17770, #9992, .T. ) ;
#4988=FACE_OUTER_BOUND ( 'NONE', #8852, .T. ) ;
#4989=DIRECTION ( 'NONE',  ( 1.000000000000000000, 0.000000000000000000, 6.123233995736764803E-17 ) ) ;
#5003=EDGE_CURVE ( 'NONE', #814, #5394, #15777, .T. ) ;
#5017=CARTESIAN_POINT ( 'NONE',  ( 33.79999999999999716, -84.70000000000001705, 1.799999999999996048 ) ) ;
#5030=CARTESIAN_POINT ( 'NONE',  ( 33.79999999999999716, -84.70000000000001705, 2.931682674400803201E-15 ) ) ;
#5039=AXIS2_PLACEMENT_3D ( 'NONE', #4050, #10863, #19942 ) ;
#5061=SHAPE_DEFINITION_REPRESENTATION ( #1428, #12850 ) ;
#5076=AXIS2_PLACEMENT_3D ( 'NONE', #6734, #11953, #317 ) ;
#5083=VERTEX_POINT ( 'NONE', #5627 ) ;
#5116=DIRECTION ( 'NONE',  ( -0.000000000000000000, 1.000000000000000000, -0.000000000000000000 ) ) ;
#5122=CARTESIAN_POINT ( 'NONE',  ( 30.19999999999999574, 70.29999999999999716, 3.992348565220370405E-15 ) ) ;
#5124=EDGE_CURVE ( 'NONE', #10124, #5205, #14142, .T. ) ;
#5134=FACE_OUTER_BOUND ( 'NONE', #17700, .T. ) ;
#5141=DIRECTION ( 'NONE',  ( 1.000000000000000000, 0.000000000000000000, 0.000000000000000000 ) ) ;
#5151=DIRECTION ( 'NONE',  ( 0.000000000000000000, 0.000000000000000000, -1.000000000000000000 ) ) ;
#5153=EDGE_CURVE ( 'NONE', #12260, #8060, #17675, .T. ) ;
#5182=FACE_OUTER_BOUND ( 'NONE', #2940, .T. ) ;
#5197=AXIS2_PLACEMENT_3D ( 'NONE', #3778, #17004, #20801 ) ;
#5204=AXIS2_PLACEMENT_3D ( 'NONE', #17581, #2246, #15879 ) ;
#5205=VERTEX_POINT ( 'NONE', #5850 ) ;
#5214=ADVANCED_FACE ( 'NONE', ( #2807 ), #20965, .T. ) ;
#5236=VECTOR ( 'NONE', #12649, 1000.000000000000000 ) ;
#5239=DIRECTION ( 'NONE',  ( 0.000000000000000000, 0.000000000000000000, 1.000000000000000000 ) ) ;
#5240=DIRECTION ( 'NONE',  ( 1.000000000000000000, 0.000000000000000000, 0.000000000000000000 ) ) ;
#5247=ORIENTED_EDGE ( 'NONE', *, *, #12958, .F. ) ;
#5252=AXIS2_PLACEMENT_3D ( 'NONE', #18345, #13538, #8187 ) ;
#5259=DIRECTION ( 'NONE',  ( -1.000000000000000000, -0.000000000000000000, 0.000000000000000000 ) ) ;
#5263=VECTOR ( 'NONE', #846, 1000.000000000000000 ) ;
#5264=CARTESIAN_POINT ( 'NONE',  ( -34.70000000000000284, 85.00000000000000000, 0.6000000000000033085 ) ) ;
#5270=EDGE_CURVE ( 'NONE', #20330, #20326, #21685, .T. ) ;
#5283=VECTOR ( 'NONE', #8991, 1000.000000000000000 ) ;
#5303=AXIS2_PLACEMENT_3D ( 'NONE', #8357, #17185, #3551 ) ;
#5314=AXIS2_PLACEMENT_3D ( 'NONE', #10021, #20310, #6667 ) ;
#5326=CARTESIAN_POINT ( 'NONE',  ( 33.19999999999999574, 84.70000000000001705, 78.79999999999999716 ) ) ;
#5330=ORIENTED_EDGE ( 'NONE', *, *, #10091, .F. ) ;
#5338=FACE_OUTER_BOUND ( 'NONE', #19332, .T. ) ;
#5346=DIRECTION ( 'NONE',  ( 1.000000000000000000, 0.000000000000000000, 0.000000000000000000 ) ) ;
#5362=FACE_OUTER_BOUND ( 'NONE', #13675, .T. ) ;
#5376=AXIS2_PLACEMENT_3D ( 'NONE', #14924, #16150, #12796 ) ;
#5394=VERTEX_POINT ( 'NONE', #10182 ) ;
#5395=ORIENTED_EDGE ( 'NONE', *, *, #14899, .F. ) ;
#5414=CARTESIAN_POINT ( 'NONE',  ( 34.69999999999999574, 84.70000000000001705, 3.009745230819759520E-15 ) ) ;
#5422=CARTESIAN_POINT ( 'NONE',  ( -30.49999999999998934, 69.70000000000001705, 1.500000000000001332 ) ) ;
#5424=ORIENTED_EDGE ( 'NONE', *, *, #21476, .T. ) ;
#5430=CARTESIAN_POINT ( 'NONE',  ( 33.79999999999999716, 84.70000000000001705, 1.799999999999996048 ) ) ;
#5432=ADVANCED_FACE ( 'NONE', ( #11713 ), #14963, .F. ) ;
#5438=DIRECTION ( 'NONE',  ( -6.123233995736764803E-17, 0.000000000000000000, 1.000000000000000000 ) ) ;
#5454=DIRECTION ( 'NONE',  ( 1.000000000000000000, 0.000000000000000000, 0.000000000000000000 ) ) ;
#5471=CARTESIAN_POINT ( 'NONE',  ( -33.20000000000001705, 85.00000000000000000, 78.79999999999999716 ) ) ;
#5474=PLANE ( 'NONE',  #8889 ) ;
#5497=ORIENTED_EDGE ( 'NONE', *, *, #733, .F. ) ;
#5502=VERTEX_POINT ( 'NONE', #8262 ) ;
#5511=( GEOMETRIC_REPRESENTATION_CONTEXT ( 3 ) GLOBAL_UNCERTAINTY_ASSIGNED_CONTEXT ( ( #19027 ) ) GLOBAL_UNIT_ASSIGNED_CONTEXT ( ( #3960, #7540, #14340 ) ) REPRESENTATION_CONTEXT ( 'NONE', 'WORKASPACE' ) );
#5520=TOROIDAL_SURFACE ( 'NONE', #8369, 0.2999999999999999889, 0.2999999999999999889 ) ;
#5536=CYLINDRICAL_SURFACE ( 'NONE', #15312, 0.2999999999999999334 ) ;
#5545=DIRECTION ( 'NONE',  ( -0.000000000000000000, 1.000000000000000000, -0.000000000000000000 ) ) ;
#5563=EDGE_CURVE ( 'NONE', #6583, #11049, #10959, .T. ) ;
#5584=TOROIDAL_SURFACE ( 'NONE', #2332, 0.5999999999999999778, 0.2999999999999999889 ) ;
#5593=EDGE_LOOP ( 'NONE', ( #15520, #11531, #7924, #14947 ) ) ;
#5602=VERTEX_POINT ( 'NONE', #6863 ) ;
#5607=ADVANCED_FACE ( 'NONE', ( #17121 ), #5584, .T. ) ;
#5610=ORIENTED_EDGE ( 'NONE', *, *, #11700, .F. ) ;
#5627=CARTESIAN_POINT ( 'NONE',  ( -30.79999999999999005, 69.70000000000001705, 1.500000000000000222 ) ) ;
#5631=AXIS2_PLACEMENT_3D ( 'NONE', #18452, #3134, #16774 ) ;
#5638=DIRECTION ( 'NONE',  ( 8.673617379884034239E-17, 0.000000000000000000, -1.000000000000000000 ) ) ;
#5657=DIRECTION ( 'NONE',  ( 0.000000000000000000, -1.000000000000000000, 0.000000000000000000 ) ) ;
#5667=DIRECTION ( 'NONE',  ( 1.000000000000000000, -0.000000000000000000, 1.734723475976806848E-16 ) ) ;
#5680=DIRECTION ( 'NONE',  ( -1.000000000000000000, 0.000000000000000000, 0.000000000000000000 ) ) ;
#5683=ADVANCED_FACE ( 'NONE', ( #3947 ), #10763, .F. ) ;
#5689=ORIENTED_EDGE ( 'NONE', *, *, #10623, .F. ) ;
#5692=AXIS2_PLACEMENT_3D ( 'NONE', #17630, #17530, #9033 ) ;
#5735=ORIENTED_EDGE ( 'NONE', *, *, #17881, .T. ) ;
#5736=CARTESIAN_POINT ( 'NONE',  ( -30.19999999999999574, 70.29999999999999716, 2.939152317953652529E-16 ) ) ;
#5738=AXIS2_PLACEMENT_3D ( 'NONE', #2447, #10940, #2657 ) ;
#5743=ADVANCED_FACE ( 'NONE', ( #982 ), #4357, .T. ) ;
#5752=AXIS2_PLACEMENT_3D ( 'NONE', #22090, #6550, #18603 ) ;
#5758=EDGE_LOOP ( 'NONE', ( #783, #12367, #1973, #18256 ) ) ;
#5762=TOROIDAL_SURFACE ( 'NONE', #3610, 0.5999999999999999778, 0.2999999999999999889 ) ;
#5764=VECTOR ( 'NONE', #6647, 1000.000000000000000 ) ;
#5800=CYLINDRICAL_SURFACE ( 'NONE', #11730, 0.2999999999999999334 ) ;
#5818=ORIENTED_EDGE ( 'NONE', *, *, #13992, .T. ) ;
#5819=AXIS2_PLACEMENT_3D ( 'NONE', #12718, #17773, #9494 ) ;
#5832=CARTESIAN_POINT ( 'NONE',  ( -33.20000000000000284, 85.00000000000000000, 1.800000000000000266 ) ) ;
#5849=CARTESIAN_POINT ( 'NONE',  ( -30.19999999999999574, 70.29999999999999716, 1.199999999999999512 ) ) ;
#5850=CARTESIAN_POINT ( 'NONE',  ( -33.20000000000001705, 84.70000000000001705, 78.50000000000000000 ) ) ;
#5858=ORIENTED_EDGE ( 'NONE', *, *, #11046, .T. ) ;
#5861=EDGE_LOOP ( 'NONE', ( #8108, #6541, #4406, #9313 ) ) ;
#5868=LINE ( 'NONE', #3856, #5236 ) ;
#5882=ORIENTED_EDGE ( 'NONE', *, *, #466, .F. ) ;
#5884=LINE ( 'NONE', #12565, #20285 ) ;
#5892=DIRECTION ( 'NONE',  ( 6.123233995736764803E-17, -0.000000000000000000, -1.000000000000000000 ) ) ;
#5898=DIRECTION ( 'NONE',  ( -1.734723475976806848E-16, 0.000000000000000000, 1.000000000000000000 ) ) ;
#5906=EDGE_CURVE ( 'NONE', #22033, #19724, #11600, .T. ) ;
#5921=DIRECTION ( 'NONE',  ( 0.000000000000000000, 0.000000000000000000, 1.000000000000000000 ) ) ;
#5930=FACE_OUTER_BOUND ( 'NONE', #17305, .T. ) ;
#5937=ORIENTED_EDGE ( 'NONE', *, *, #17035, .F. ) ;
#5957=EDGE_CURVE ( 'NONE', #21291, #1963, #18665, .T. ) ;
#5961=VECTOR ( 'NONE', #632, 1000.000000000000000 ) ;
#5969=CARTESIAN_POINT ( 'NONE',  ( 30.49999999999999645, 70.29999999999999716, 1.200000000000003064 ) ) ;
#6007=CARTESIAN_POINT ( 'NONE',  ( -30.19999999999999574, 70.29999999999999716, 0.3000000000000002665 ) ) ;
#6012=AXIS2_PLACEMENT_3D ( 'NONE', #15086, #20137, #5141 ) ;
#6014=LINE ( 'NONE', #9796, #19490 ) ;
#6016=CARTESIAN_POINT ( 'NONE',  ( -35.00000000000001421, -84.70000000000001705, 78.50000000000000000 ) ) ;
#6017=DIRECTION ( 'NONE',  ( 0.000000000000000000, 0.000000000000000000, -1.000000000000000000 ) ) ;
#6021=ORIENTED_EDGE ( 'NONE', *, *, #15249, .T. ) ;
#6026=ADVANCED_FACE ( 'NONE', ( #14162 ), #10602, .F. ) ;
#6029=DIRECTION ( 'NONE',  ( 0.000000000000000000, -1.000000000000000000, 0.000000000000000000 ) ) ;
#6033=CARTESIAN_POINT ( 'NONE',  ( -33.20000000000001705, -85.00000000000000000, 78.20000000000000284 ) ) ;
#6039=CIRCLE ( 'NONE', #2083, 0.2999999999999999334 ) ;
#6045=DIRECTION ( 'NONE',  ( -0.000000000000000000, -1.000000000000000000, -0.000000000000000000 ) ) ;
#6046=CARTESIAN_POINT ( 'NONE',  ( -34.70000000000001705, -84.70000000000001705, 79.39999999999999147 ) ) ;
#6068=DIRECTION ( 'NONE',  ( 1.000000000000000000, 0.000000000000000000, 0.000000000000000000 ) ) ;
#6092=EDGE_CURVE ( 'NONE', #675, #17770, #2322, .T. ) ;
#6125=CARTESIAN_POINT ( 'NONE',  ( 30.49999999999999645, 70.00000000000000000, 0.3000000000000033751 ) ) ;
#6155=DIRECTION ( 'NONE',  ( 1.000000000000000000, 0.000000000000000000, 0.000000000000000000 ) ) ;
#6158=TOROIDAL_SURFACE ( 'NONE', #5076, 0.2999999999999999889, 0.2999999999999999889 ) ;
#6160=CARTESIAN_POINT ( 'NONE',  ( 30.79999999999999716, 69.70000000000000284, 1.500000000000004219 ) ) ;
#6174=AXIS2_PLACEMENT_3D ( 'NONE', #7636, #794, #1220 ) ;
#6175=VERTEX_POINT ( 'NONE', #9588 ) ;
#6177=DIRECTION ( 'NONE',  ( 0.000000000000000000, 0.000000000000000000, -1.000000000000000000 ) ) ;
#6198=VECTOR ( 'NONE', #18604, 1000.000000000000000 ) ;
#6213=EDGE_CURVE ( 'NONE', #15018, #20326, #6467, .T. ) ;
#6228=DIRECTION ( 'NONE',  ( 0.000000000000000000, 0.000000000000000000, -1.000000000000000000 ) ) ;
#6235=CYLINDRICAL_SURFACE ( 'NONE', #21607, 0.3000000000000016542 ) ;
#6256=CARTESIAN_POINT ( 'NONE',  ( 34.39999999999998437, 85.00000000000000000, 79.39999999999999147 ) ) ;
#6263=CYLINDRICAL_SURFACE ( 'NONE', #2454, 0.2999999999999947153 ) ;
#6271=ORIENTED_EDGE ( 'NONE', *, *, #21179, .F. ) ;
#6300=( NAMED_UNIT ( * ) PLANE_ANGLE_UNIT ( ) SI_UNIT ( $, .RADIAN. ) );
#6308=ADVANCED_FACE ( 'NONE', ( #15387 ), #60, .T. ) ;
#6335=AXIS2_PLACEMENT_3D ( 'NONE', #8304, #3153, #8524 ) ;
#6337=ADVANCED_FACE ( 'NONE', ( #5338 ), #15487, .T. ) ;
#6342=CARTESIAN_POINT ( 'NONE',  ( -33.20000000000000284, -85.00000000000000000, 1.800000000000000266 ) ) ;
#6344=CIRCLE ( 'NONE', #15250, 0.2999999999999999889 ) ;
#6353=ORIENTED_EDGE ( 'NONE', *, *, #15726, .T. ) ;
#6370=EDGE_CURVE ( 'NONE', #21952, #12463, #904, .T. ) ;
#6407=AXIS2_PLACEMENT_3D ( 'NONE', #180, #10594, #7034 ) ;
#6412=CARTESIAN_POINT ( 'NONE',  ( 30.49999999999999645, 69.70000000000000284, 1.200000000000003064 ) ) ;
#6420=DIRECTION ( 'NONE',  ( 1.000000000000000000, 0.000000000000000000, 6.123233995736764803E-17 ) ) ;
#6425=UNCERTAINTY_MEASURE_WITH_UNIT (LENGTH_MEASURE( 1.000000000000000082E-05 ), #8577, 'distance_accuracy_value', 'NONE');
#6428=ORIENTED_EDGE ( 'NONE', *, *, #20299, .F. ) ;
#6435=ORIENTED_EDGE ( 'NONE', *, *, #6830, .T. ) ;
#6467=LINE ( 'NONE', #9914, #7713 ) ;
#6480=EDGE_CURVE ( 'NONE', #15917, #10124, #918, .T. ) ;
#6491=DIRECTION ( 'NONE',  ( -0.000000000000000000, 1.000000000000000000, -0.000000000000000000 ) ) ;
#6493=EDGE_CURVE ( 'NONE', #18912, #10431, #13418, .T. ) ;
#6502=CARTESIAN_POINT ( 'NONE',  ( -34.39999999999999858, -85.00000000000000000, 0.6000000000000033085 ) ) ;
#6506=EDGE_LOOP ( 'NONE', ( #216, #14457, #482, #16653 ) ) ;
#6507=TOROIDAL_SURFACE ( 'NONE', #12902, 0.5999999999999999778, 0.2999999999999999889 ) ;
#6541=ORIENTED_EDGE ( 'NONE', *, *, #18026, .F. ) ;
#6543=ORIENTED_EDGE ( 'NONE', *, *, #14223, .T. ) ;
#6550=DIRECTION ( 'NONE',  ( -0.000000000000000000, -0.000000000000000000, -1.000000000000000000 ) ) ;
#6583=VERTEX_POINT ( 'NONE', #16135 ) ;
#6609=VERTEX_POINT ( 'NONE', #16578 ) ;
#6636=ORIENTED_EDGE ( 'NONE', *, *, #1594, .T. ) ;
#6647=DIRECTION ( 'NONE',  ( 1.000000000000000000, -0.000000000000000000, 6.123233995736764803E-17 ) ) ;
#6659=LINE ( 'NONE', #3394, #7432 ) ;
#6667=DIRECTION ( 'NONE',  ( -6.123233995736764803E-17, 0.000000000000000000, 1.000000000000000000 ) ) ;
#6685=CIRCLE ( 'NONE', #11301, 0.5999999999999999778 ) ;
#6690=DIRECTION ( 'NONE',  ( 1.000000000000000000, 0.000000000000000000, 0.000000000000000000 ) ) ;
#6697=LINE ( 'NONE', #3431, #4698 ) ;
#6698=VERTEX_POINT ( 'NONE', #13339 ) ;
#6701=CARTESIAN_POINT ( 'NONE',  ( -33.20000000000000284, -85.00000000000000000, 1.200000000000000400 ) ) ;
#6711=CIRCLE ( 'NONE', #14177, 0.2999999999999947153 ) ;
#6718=DIRECTION ( 'NONE',  ( 0.000000000000000000, -1.000000000000000000, 0.000000000000000000 ) ) ;
#6719=DIRECTION ( 'NONE',  ( 0.000000000000000000, -1.000000000000000000, 0.000000000000000000 ) ) ;
#6729=AXIS2_PLACEMENT_3D ( 'NONE', #4643, #9445, #21769 ) ;
#6734=CARTESIAN_POINT ( 'NONE',  ( -34.40000000000001279, -84.70000000000001705, 79.39999999999999147 ) ) ;
#6745=CIRCLE ( 'NONE', #14219, 0.2999999999999999889 ) ;
#6760=VECTOR ( 'NONE', #15869, 1000.000000000000000 ) ;
#6761=ORIENTED_EDGE ( 'NONE', *, *, #466, .T. ) ;
#6767=PLANE ( 'NONE',  #16092 ) ;
#6771=CIRCLE ( 'NONE', #12797, 0.2999999999999999889 ) ;
#6774=AXIS2_PLACEMENT_3D ( 'NONE', #16502, #1167, #19996 ) ;
#6778=DIRECTION ( 'NONE',  ( 1.000000000000000000, 0.000000000000000000, 6.123233995736764803E-17 ) ) ;
#6782=EDGE_CURVE ( 'NONE', #341, #4617, #20628, .T. ) ;
#6800=DIRECTION ( 'NONE',  ( 0.000000000000000000, 0.000000000000000000, -1.000000000000000000 ) ) ;
#6815=EDGE_CURVE ( 'NONE', #15052, #3842, #18751, .T. ) ;
#6823=DIRECTION ( 'NONE',  ( -6.123233995736764803E-17, 0.000000000000000000, 1.000000000000000000 ) ) ;
#6830=EDGE_CURVE ( 'NONE', #4063, #20326, #14806, .T. ) ;
#6832=FACE_OUTER_BOUND ( 'NONE', #2700, .T. ) ;
#6840=VERTEX_POINT ( 'NONE', #12748 ) ;
#6843=CIRCLE ( 'NONE', #12150, 0.3000000000000016542 ) ;
#6850=CARTESIAN_POINT ( 'NONE',  ( -34.39999999999999858, -85.00000000000000000, 0.3000000000000000444 ) ) ;
#6859=ADVANCED_FACE ( 'NONE', ( #16111 ), #4382, .F. ) ;
#6863=CARTESIAN_POINT ( 'NONE',  ( 34.69999999999999574, 85.00000000000000000, 0.6000000000000037526 ) ) ;
#6875=DIRECTION ( 'NONE',  ( 0.000000000000000000, -1.000000000000000000, 0.000000000000000000 ) ) ;
#6877=DIRECTION ( 'NONE',  ( 0.000000000000000000, -0.000000000000000000, 1.000000000000000000 ) ) ;
#6889=EDGE_LOOP ( 'NONE', ( #7898, #6428, #1290, #390 ) ) ;
#6892=CARTESIAN_POINT ( 'NONE',  ( -7.347880794884131322E-17, -84.70000000000001705, 1.200000000000002176 ) ) ;
#6901=DIRECTION ( 'NONE',  ( -1.000000000000000000, 0.000000000000000000, 0.000000000000000000 ) ) ;
#6902=DIRECTION ( 'NONE',  ( -6.123233995736764803E-17, 0.000000000000000000, 1.000000000000000000 ) ) ;
#6903=ORIENTED_EDGE ( 'NONE', *, *, #3235, .T. ) ;
#6908=DIRECTION ( 'NONE',  ( -1.000000000000000000, 0.000000000000000000, -6.123233995736764803E-17 ) ) ;
#6914=CYLINDRICAL_SURFACE ( 'NONE', #11104, 0.3000000000000016542 ) ;
#6917=ORIENTED_EDGE ( 'NONE', *, *, #6974, .T. ) ;
#6929=CARTESIAN_POINT ( 'NONE',  ( 30.79999999999999716, -84.70000000000001705, 0.3000000000000039857 ) ) ;
#6943=CARTESIAN_POINT ( 'NONE',  ( 33.49999999999998579, 85.00000000000000000, 78.20000000000000284 ) ) ;
#6947=CARTESIAN_POINT ( 'NONE',  ( -33.50000000000001421, 85.00000000000000000, 78.79999999999999716 ) ) ;
#6954=LINE ( 'NONE', #3690, #2932 ) ;
#6958=EDGE_CURVE ( 'NONE', #6698, #12463, #19822, .T. ) ;
#6971=VERTEX_POINT ( 'NONE', #4485 ) ;
#6974=EDGE_CURVE ( 'NONE', #17660, #4505, #13318, .T. ) ;
#6977=ORIENTED_EDGE ( 'NONE', *, *, #10120, .F. ) ;
#6991=ORIENTED_EDGE ( 'NONE', *, *, #13157, .T. ) ;
#6992=AXIS2_PLACEMENT_3D ( 'NONE', #13155, #4332, #11144 ) ;
#7001=VERTEX_POINT ( 'NONE', #4937 ) ;
#7032=ORIENTED_EDGE ( 'NONE', *, *, #10120, .T. ) ;
#7034=DIRECTION ( 'NONE',  ( 1.000000000000000000, 0.000000000000000000, 0.000000000000000000 ) ) ;
#7036=CARTESIAN_POINT ( 'NONE',  ( 34.69999999999999574, 84.70000000000001705, 0.6000000000000037526 ) ) ;
#7053=AXIS2_PLACEMENT_3D ( 'NONE', #6342, #21785, #1166 ) ;
#7072=TOROIDAL_SURFACE ( 'NONE', #6729, 0.5999999999999999778, 0.2999999999999999889 ) ;
#7095=CARTESIAN_POINT ( 'NONE',  ( 30.49999999999999645, 69.70000000000000284, 0.3000000000000033751 ) ) ;
#7105=LINE ( 'NONE', #19166, #5283 ) ;
#7112=AXIS2_PLACEMENT_3D ( 'NONE', #6033, #12818, #17975 ) ;
#7127=EDGE_CURVE ( 'NONE', #17668, #14491, #19109, .T. ) ;
#7139=DIRECTION ( 'NONE',  ( 1.000000000000000000, 0.000000000000000000, 0.000000000000000000 ) ) ;
#7150=ORIENTED_EDGE ( 'NONE', *, *, #5003, .F. ) ;
#7174=EDGE_CURVE ( 'NONE', #814, #3057, #14093, .T. ) ;
#7205=DIRECTION ( 'NONE',  ( 0.000000000000000000, 0.000000000000000000, 1.000000000000000000 ) ) ;
#7207=ORIENTED_EDGE ( 'NONE', *, *, #18196, .F. ) ;
#7234=ORIENTED_EDGE ( 'NONE', *, *, #13157, .F. ) ;
#7243=PLANE ( 'NONE',  #21513 ) ;
#7246=CARTESIAN_POINT ( 'NONE',  ( -30.19999999999999574, 69.70000000000001705, 1.500000000000000222 ) ) ;
#7249=CARTESIAN_POINT ( 'NONE',  ( 33.79999999999999005, 84.70000000000001705, 78.20000000000000284 ) ) ;
#7281=DIRECTION ( 'NONE',  ( -8.673617379884034239E-17, -0.000000000000000000, 1.000000000000000000 ) ) ;
#7292=ADVANCED_FACE ( 'NONE', ( #958 ), #4224, .T. ) ;
#7303=CIRCLE ( 'NONE', #17649, 0.2999999999999999334 ) ;
#7323=DIRECTION ( 'NONE',  ( 0.000000000000000000, 0.000000000000000000, -1.000000000000000000 ) ) ;
#7329=DIRECTION ( 'NONE',  ( 0.000000000000000000, 0.000000000000000000, 1.000000000000000000 ) ) ;
#7336=ORIENTED_EDGE ( 'NONE', *, *, #3701, .F. ) ;
#7342=DIRECTION ( 'NONE',  ( -0.000000000000000000, 1.000000000000000000, -0.000000000000000000 ) ) ;
#7347=DIRECTION ( 'NONE',  ( 1.000000000000000000, 0.000000000000000000, 0.000000000000000000 ) ) ;
#7360=DIRECTION ( 'NONE',  ( 0.000000000000000000, 0.000000000000000000, -1.000000000000000000 ) ) ;
#7396=EDGE_LOOP ( 'NONE', ( #11012, #15796, #540, #8434, #21317, #2191, #18209, #21859, #18582, #19553 ) ) ;
#7397=AXIS2_PLACEMENT_3D ( 'NONE', #18088, #1190, #13045 ) ;
#7405=DIRECTION ( 'NONE',  ( 1.000000000000000000, 0.000000000000000000, 0.000000000000000000 ) ) ;
#7429=AXIS2_PLACEMENT_3D ( 'NONE', #10523, #2003, #7512 ) ;
#7432=VECTOR ( 'NONE', #11779, 1000.000000000000000 ) ;
#7475=ORIENTED_EDGE ( 'NONE', *, *, #2901, .T. ) ;
#7512=DIRECTION ( 'NONE',  ( 0.000000000000000000, 0.000000000000000000, 1.000000000000000000 ) ) ;
#7516=CARTESIAN_POINT ( 'NONE',  ( 34.39999999999998437, -84.70000000000001705, 4.249524393041314059E-15 ) ) ;
#7517=CIRCLE ( 'NONE', #2128, 0.3000000000000016542 ) ;
#7523=DIRECTION ( 'NONE',  ( -0.000000000000000000, 1.000000000000000000, -0.000000000000000000 ) ) ;
#7525=CARTESIAN_POINT ( 'NONE',  ( 33.79999999999999005, 85.00000000000000000, 78.20000000000000284 ) ) ;
#7540=( NAMED_UNIT ( * ) PLANE_ANGLE_UNIT ( ) SI_UNIT ( $, .RADIAN. ) );
#7550=EDGE_LOOP ( 'NONE', ( #20728, #13342, #19464, #2033 ) ) ;
#7553=FACE_OUTER_BOUND ( 'NONE', #15169, .T. ) ;
#7558=DIRECTION ( 'NONE',  ( -1.000000000000000000, 0.000000000000000000, -6.123233995736764803E-17 ) ) ;
#7567=CIRCLE ( 'NONE', #69, 0.2999999999999999889 ) ;
#7569=AXIS2_PLACEMENT_3D ( 'NONE', #1041, #16367, #14906 ) ;
#7572=FACE_OUTER_BOUND ( 'NONE', #12006, .T. ) ;
#7583=CARTESIAN_POINT ( 'NONE',  ( -34.70000000000000284, 84.70000000000001705, -6.019490461639519829E-15 ) ) ;
#7587=ORIENTED_EDGE ( 'NONE', *, *, #5906, .F. ) ;
#7599=VERTEX_POINT ( 'NONE', #20769 ) ;
#7614=VECTOR ( 'NONE', #11446, 1000.000000000000000 ) ;
#7616=DIRECTION ( 'NONE',  ( 0.000000000000000000, 1.000000000000000000, 0.000000000000000000 ) ) ;
#7619=CARTESIAN_POINT ( 'NONE',  ( 34.39999999999998437, 85.00000000000000000, 4.249524393041314059E-15 ) ) ;
#7628=DIRECTION ( 'NONE',  ( -8.673617379884034239E-17, 0.000000000000000000, 1.000000000000000000 ) ) ;
#7630=EDGE_CURVE ( 'NONE', #6698, #15951, #4513, .T. ) ;
#7634=DIRECTION ( 'NONE',  ( 0.000000000000000000, -1.000000000000000000, 0.000000000000000000 ) ) ;
#7636=CARTESIAN_POINT ( 'NONE',  ( -30.79999999999999361, -84.70000000000001705, 0.3000000000000002665 ) ) ;
#7672=CYLINDRICAL_SURFACE ( 'NONE', #20962, 0.2999999999999947153 ) ;
#7705=EDGE_CURVE ( 'NONE', #21689, #12623, #924, .T. ) ;
#7712=VECTOR ( 'NONE', #14213, 1000.000000000000000 ) ;
#7713=VECTOR ( 'NONE', #13367, 1000.000000000000000 ) ;
#7718=LINE ( 'NONE', #11067, #17408 ) ;
#7720=EDGE_CURVE ( 'NONE', #12463, #20684, #1046, .T. ) ;
#7735=DIRECTION ( 'NONE',  ( -8.673617379884034239E-17, -0.000000000000000000, 1.000000000000000000 ) ) ;
#7741=DIRECTION ( 'NONE',  ( 0.000000000000000000, 1.000000000000000000, 0.000000000000000000 ) ) ;
#7747=ORIENTED_EDGE ( 'NONE', *, *, #8118, .F. ) ;
#7763=LINE ( 'NONE', #2710, #920 ) ;
#7786=FACE_OUTER_BOUND ( 'NONE', #1854, .T. ) ;
#7819=CYLINDRICAL_SURFACE ( 'NONE', #608, 0.2999999999999999889 ) ;
#7827=CYLINDRICAL_SURFACE ( 'NONE', #13955, 0.6000000000000033085 ) ;
#7845=CARTESIAN_POINT ( 'NONE',  ( -30.79999999999999361, -84.70000000000001705, 2.571758278209446887E-16 ) ) ;
#7852=ORIENTED_EDGE ( 'NONE', *, *, #11893, .F. ) ;
#7855=VERTEX_POINT ( 'NONE', #7525 ) ;
#7859=CARTESIAN_POINT ( 'NONE',  ( 30.19999999999999574, 70.29999999999999716, 1.500000000000003997 ) ) ;
#7869=AXIS2_PLACEMENT_3D ( 'NONE', #5017, #1530, #14964 ) ;
#7871=DIRECTION ( 'NONE',  ( -1.734723475976806848E-16, 0.000000000000000000, 1.000000000000000000 ) ) ;
#7876=EDGE_CURVE ( 'NONE', #9461, #4063, #2137, .T. ) ;
#7881=CIRCLE ( 'NONE', #20387, 0.2999999999999999334 ) ;
#7886=EDGE_CURVE ( 'NONE', #22033, #341, #4493, .T. ) ;
#7898=ORIENTED_EDGE ( 'NONE', *, *, #6958, .T. ) ;
#7904=ORIENTED_EDGE ( 'NONE', *, *, #21020, .T. ) ;
#7924=ORIENTED_EDGE ( 'NONE', *, *, #6370, .F. ) ;
#7975=CARTESIAN_POINT ( 'NONE',  ( 33.79999999999999005, -84.70000000000001705, 78.20000000000000284 ) ) ;
#8004=ORIENTED_EDGE ( 'NONE', *, *, #6493, .F. ) ;
#8005=MECHANICAL_DESIGN_GEOMETRIC_PRESENTATION_REPRESENTATION('',(#17264),#19416);
#8007=CARTESIAN_POINT ( 'NONE',  ( 34.69999999999998863, -85.00000000000000000, 0.6000000000000033085 ) ) ;
#8012=CARTESIAN_POINT ( 'NONE',  ( 30.79999999999999716, -84.70000000000001705, 1.200000000000004174 ) ) ;
#8024=CIRCLE ( 'NONE', #3212, 0.2999999999999999889 ) ;
#8029=DIRECTION ( 'NONE',  ( -6.123233995736764803E-17, 0.000000000000000000, 1.000000000000000000 ) ) ;
#8032=CARTESIAN_POINT ( 'NONE',  ( 34.99999999999999289, 84.70000000000001705, 0.6000000000000033085 ) ) ;
#8037=CARTESIAN_POINT ( 'NONE',  ( 33.19999999999999574, -85.00000000000000000, 78.50000000000000000 ) ) ;
#8058=PLANE ( 'NONE',  #11668 ) ;
#8060=VERTEX_POINT ( 'NONE', #1792 ) ;
#8078=ORIENTED_EDGE ( 'NONE', *, *, #1491, .T. ) ;
#8082=VERTEX_POINT ( 'NONE', #6850 ) ;
#8086=SHAPE_REPRESENTATION_RELATIONSHIP ( 'NONE' , 'NONE' ,  #12850, #13111 ) ;
#8107=EDGE_LOOP ( 'NONE', ( #19396, #13816, #14032, #16011 ) ) ;
#8108=ORIENTED_EDGE ( 'NONE', *, *, #11877, .T. ) ;
#8118=EDGE_CURVE ( 'NONE', #10999, #13328, #9225, .T. ) ;
#8121=CIRCLE ( 'NONE', #21352, 0.2999999999999999889 ) ;
#8140=ORIENTED_EDGE ( 'NONE', *, *, #3228, .T. ) ;
#8145=VERTEX_POINT ( 'NONE', #11616 ) ;
#8155=DIRECTION ( 'NONE',  ( 1.000000000000000000, 0.000000000000000000, 0.000000000000000000 ) ) ;
#8158=AXIS2_PLACEMENT_3D ( 'NONE', #1752, #20449, #11581 ) ;
#8164=ORIENTED_EDGE ( 'NONE', *, *, #7705, .T. ) ;
#8168=DIRECTION ( 'NONE',  ( -1.000000000000000000, 0.000000000000000000, -8.673617379883930701E-17 ) ) ;
#8180=ADVANCED_FACE ( 'NONE', ( #22056 ), #15635, .T. ) ;
#8185=CARTESIAN_POINT ( 'NONE',  ( 33.19999999999999574, 84.70000000000001705, 78.20000000000000284 ) ) ;
#8187=DIRECTION ( 'NONE',  ( 0.000000000000000000, 0.000000000000000000, -1.000000000000000000 ) ) ;
#8200=DIRECTION ( 'NONE',  ( 1.000000000000000000, 0.000000000000000000, 0.000000000000000000 ) ) ;
#8205=ORIENTED_EDGE ( 'NONE', *, *, #11769, .T. ) ;
#8208=ORIENTED_EDGE ( 'NONE', *, *, #1580, .F. ) ;
#8224=FACE_OUTER_BOUND ( 'NONE', #6889, .T. ) ;
#8251=DIRECTION ( 'NONE',  ( 1.000000000000000000, 0.000000000000000000, 0.000000000000000000 ) ) ;
#8262=CARTESIAN_POINT ( 'NONE',  ( 34.39999999999998437, 84.70000000000001705, 4.249524393041314059E-15 ) ) ;
#8279=EDGE_LOOP ( 'NONE', ( #14698, #2849, #11373, #968 ) ) ;
#8289=LINE ( 'NONE', #19810, #4190 ) ;
#8295=DIRECTION ( 'NONE',  ( -0.000000000000000000, 1.000000000000000000, -0.000000000000000000 ) ) ;
#8297=DIRECTION ( 'NONE',  ( 0.000000000000000000, 0.000000000000000000, 1.000000000000000000 ) ) ;
#8304=CARTESIAN_POINT ( 'NONE',  ( -34.70000000000001705, 84.70000000000001705, 79.39999999999999147 ) ) ;
#8305=AXIS2_PLACEMENT_3D ( 'NONE', #6046, #5921, #17652 ) ;
#8314=ORIENTED_EDGE ( 'NONE', *, *, #9612, .F. ) ;
#8317=CARTESIAN_POINT ( 'NONE',  ( -34.40000000000001279, 85.00000000000000000, 79.39999999999999147 ) ) ;
#8320=DIRECTION ( 'NONE',  ( 0.000000000000000000, 1.000000000000000000, 0.000000000000000000 ) ) ;
#8327=ORIENTED_EDGE ( 'NONE', *, *, #11988, .F. ) ;
#8344=SURFACE_STYLE_FILL_AREA ( #18740 ) ;
#8352=ORIENTED_EDGE ( 'NONE', *, *, #12349, .F. ) ;
#8354=DIRECTION ( 'NONE',  ( 0.000000000000000000, 0.000000000000000000, -1.000000000000000000 ) ) ;
#8357=CARTESIAN_POINT ( 'NONE',  ( 33.19999999999999574, 84.70000000000001705, 1.799999999999996048 ) ) ;
#8369=AXIS2_PLACEMENT_3D ( 'NONE', #13421, #11747, #10086 ) ;
#8383=FACE_OUTER_BOUND ( 'NONE', #7396, .T. ) ;
#8384=ORIENTED_EDGE ( 'NONE', *, *, #15664, .T. ) ;
#8394=ADVANCED_FACE ( 'NONE', ( #4122 ), #6263, .T. ) ;
#8397=CARTESIAN_POINT ( 'NONE',  ( 34.39999999999998437, -84.70000000000001705, 80.00000000000000000 ) ) ;
#8421=EDGE_CURVE ( 'NONE', #12280, #5602, #18217, .T. ) ;
#8434=ORIENTED_EDGE ( 'NONE', *, *, #7720, .T. ) ;
#8467=FACE_OUTER_BOUND ( 'NONE', #4641, .T. ) ;
#8489=LINE ( 'NONE', #13290, #16669 ) ;
#8503=TOROIDAL_SURFACE ( 'NONE', #15214, 0.2999999999999999889, 0.2999999999999999889 ) ;
#8524=DIRECTION ( 'NONE',  ( -1.000000000000000000, 0.000000000000000000, 0.000000000000000000 ) ) ;
#8555=ORIENTED_EDGE ( 'NONE', *, *, #10842, .T. ) ;
#8567=EDGE_CURVE ( 'NONE', #13921, #4692, #18428, .T. ) ;
#8577=( LENGTH_UNIT ( ) NAMED_UNIT ( * ) SI_UNIT ( .MILLI., .METRE. ) );
#8589=DIRECTION ( 'NONE',  ( 0.000000000000000000, 0.000000000000000000, -1.000000000000000000 ) ) ;
#8603=DIRECTION ( 'NONE',  ( 1.000000000000000000, 0.000000000000000000, 0.000000000000000000 ) ) ;
#8610=CYLINDRICAL_SURFACE ( 'NONE', #2468, 0.3000000000000016542 ) ;
#8639=ADVANCED_FACE ( 'NONE', ( #5362 ), #22122, .T. ) ;
#8641=VERTEX_POINT ( 'NONE', #5471 ) ;
#8653=DIRECTION ( 'NONE',  ( 0.000000000000000000, 0.000000000000000000, -1.000000000000000000 ) ) ;
#8664=ADVANCED_FACE ( 'NONE', ( #10819 ), #15508, .T. ) ;
#8678=CARTESIAN_POINT ( 'NONE',  ( -34.40000000000001279, -84.70000000000001705, 79.70000000000000284 ) ) ;
#8688=DIRECTION ( 'NONE',  ( -0.000000000000000000, 1.000000000000000000, -0.000000000000000000 ) ) ;
#8705=ADVANCED_FACE ( 'NONE', ( #11359 ), #5800, .T. ) ;
#8715=DIRECTION ( 'NONE',  ( 0.000000000000000000, -1.000000000000000000, 0.000000000000000000 ) ) ;
#8765=LINE ( 'NONE', #14103, #17094 ) ;
#8794=CYLINDRICAL_SURFACE ( 'NONE', #1343, 0.2999999999999999889 ) ;
#8795=EDGE_CURVE ( 'NONE', #9891, #18983, #14378, .T. ) ;
#8833=ORIENTED_EDGE ( 'NONE', *, *, #4167, .T. ) ;
#8852=EDGE_LOOP ( 'NONE', ( #17915, #5424, #6271 ) ) ;
#8854=AXIS2_PLACEMENT_3D ( 'NONE', #15281, #5116, #11916 ) ;
#8859=EDGE_CURVE ( 'NONE', #5394, #17668, #2102, .T. ) ;
#8864=ADVANCED_FACE ( 'NONE', ( #4988 ), #3195, .T. ) ;
#8867=DIRECTION ( 'NONE',  ( -1.000000000000000000, 0.000000000000000000, 0.000000000000000000 ) ) ;
#8869=LINE ( 'NONE', #1914, #20755 ) ;
#8872=CARTESIAN_POINT ( 'NONE',  ( 34.69999999999998863, -85.00000000000000000, 79.39999999999999147 ) ) ;
#8873=DIRECTION ( 'NONE',  ( 0.000000000000000000, -1.000000000000000000, 0.000000000000000000 ) ) ;
#8889=AXIS2_PLACEMENT_3D ( 'NONE', #1771, #20356, #10598 ) ;
#8906=ORIENTED_EDGE ( 'NONE', *, *, #15014, .F. ) ;
#8907=CARTESIAN_POINT ( 'NONE',  ( 30.49999999999999645, 70.00000000000001421, 1.200000000000003064 ) ) ;
#8925=DIRECTION ( 'NONE',  ( 1.000000000000000000, 0.000000000000000000, -0.000000000000000000 ) ) ;
#8958=ADVANCED_FACE ( 'NONE', ( #21786 ), #18921, .T. ) ;
#8979=DIRECTION ( 'NONE',  ( 1.000000000000000000, -0.000000000000000000, 6.123233995736764803E-17 ) ) ;
#8980=DIRECTION ( 'NONE',  ( 0.000000000000000000, 0.000000000000000000, 1.000000000000000000 ) ) ;
#8991=DIRECTION ( 'NONE',  ( -1.788744114411106313E-17, -1.000000000000000000, -1.095289877103613968E-33 ) ) ;
#9023=ORIENTED_EDGE ( 'NONE', *, *, #15004, .F. ) ;
#9025=CARTESIAN_POINT ( 'NONE',  ( -30.19999999999999574, 70.00000000000000000, 1.199999999999999512 ) ) ;
#9033=DIRECTION ( 'NONE',  ( 0.000000000000000000, 0.000000000000000000, -1.000000000000000000 ) ) ;
#9037=EDGE_LOOP ( 'NONE', ( #19975, #10609, #5395, #19108 ) ) ;
#9041=DIRECTION ( 'NONE',  ( -1.000000000000000000, 0.000000000000000000, -6.123233995736764803E-17 ) ) ;
#9065=LINE ( 'NONE', #15984, #6760 ) ;
#9091=LINE ( 'NONE', #5422, #13110 ) ;
#9097=FACE_OUTER_BOUND ( 'NONE', #5593, .T. ) ;
#9121=CARTESIAN_POINT ( 'NONE',  ( 30.19999999999999574, 70.00000000000000000, 0.3000000000000033751 ) ) ;
#9129=AXIS2_PLACEMENT_3D ( 'NONE', #15271, #20002, #6800 ) ;
#9131=AXIS2_PLACEMENT_3D ( 'NONE', #11235, #18059, #21666 ) ;
#9141=PLANE ( 'NONE',  #19518 ) ;
#9143=VERTEX_POINT ( 'NONE', #19817 ) ;
#9184=CYLINDRICAL_SURFACE ( 'NONE', #2893, 0.3000000000000016542 ) ;
#9186=CARTESIAN_POINT ( 'NONE',  ( 34.99999999999999289, 84.70000000000001705, 80.00000000000000000 ) ) ;
#9187=DIRECTION ( 'NONE',  ( 0.000000000000000000, 0.000000000000000000, -1.000000000000000000 ) ) ;
#9207=TOROIDAL_SURFACE ( 'NONE', #5303, 0.5999999999999999778, 0.2999999999999999889 ) ;
#9208=TOROIDAL_SURFACE ( 'NONE', #12061, 0.5999999999999999778, 0.2999999999999999889 ) ;
#9209=CIRCLE ( 'NONE', #4923, 0.3000000000000016542 ) ;
#9213=DIRECTION ( 'NONE',  ( 1.000000000000000000, -0.000000000000000000, 6.123233995736764803E-17 ) ) ;
#9225=CIRCLE ( 'NONE', #14563, 0.2999999999999947153 ) ;
#9246=VECTOR ( 'NONE', #11996, 1000.000000000000000 ) ;
#9271=VERTEX_POINT ( 'NONE', #12069 ) ;
#9289=DIRECTION ( 'NONE',  ( 1.000000000000000000, -0.000000000000000000, -0.000000000000000000 ) ) ;
#9313=ORIENTED_EDGE ( 'NONE', *, *, #16871, .F. ) ;
#9334=ORIENTED_EDGE ( 'NONE', *, *, #19141, .F. ) ;
#9369=AXIS2_PLACEMENT_3D ( 'NONE', #16544, #12626, #10466 ) ;
#9378=AXIS2_PLACEMENT_3D ( 'NONE', #20823, #12177, #12509 ) ;
#9382=DIRECTION ( 'NONE',  ( 0.000000000000000000, 0.000000000000000000, 1.000000000000000000 ) ) ;
#9423=SURFACE_SIDE_STYLE ('',( #17917 ) ) ;
#9426=ORIENTED_EDGE ( 'NONE', *, *, #4167, .F. ) ;
#9445=DIRECTION ( 'NONE',  ( -6.123233995736764803E-17, 0.000000000000000000, 1.000000000000000000 ) ) ;
#9461=VERTEX_POINT ( 'NONE', #3694 ) ;
#9481=CYLINDRICAL_SURFACE ( 'NONE', #2414, 0.5999999999999999778 ) ;
#9494=DIRECTION ( 'NONE',  ( 0.000000000000000000, 0.000000000000000000, -1.000000000000000000 ) ) ;
#9499=DIRECTION ( 'NONE',  ( 1.000000000000000000, -0.000000000000000000, -0.000000000000000000 ) ) ;
#9513=CARTESIAN_POINT ( 'NONE',  ( 0.000000000000000000, -85.00000000000000000, 0.000000000000000000 ) ) ;
#9523=VECTOR ( 'NONE', #15484, 1000.000000000000000 ) ;
#9546=AXIS2_PLACEMENT_3D ( 'NONE', #18638, #1751, #13808 ) ;
#9552=DIRECTION ( 'NONE',  ( -1.734723475976806848E-16, 0.000000000000000000, 1.000000000000000000 ) ) ;
#9553=ADVANCED_FACE ( 'NONE', ( #3322 ), #3426, .F. ) ;
#9584=AXIS2_PLACEMENT_3D ( 'NONE', #10740, #17321, #648 ) ;
#9587=ORIENTED_EDGE ( 'NONE', *, *, #16432, .T. ) ;
#9588=CARTESIAN_POINT ( 'NONE',  ( 33.49999999999999289, 84.70000000000001705, 1.799999999999996048 ) ) ;
#9599=FACE_OUTER_BOUND ( 'NONE', #2885, .T. ) ;
#9601=CIRCLE ( 'NONE', #14895, 0.3000000000000016542 ) ;
#9612=EDGE_CURVE ( 'NONE', #5394, #583, #18220, .T. ) ;
#9615=DIRECTION ( 'NONE',  ( -1.000000000000000000, 0.000000000000000000, 0.000000000000000000 ) ) ;
#9635=EDGE_LOOP ( 'NONE', ( #11738, #3162, #11599, #20572, #18982, #20876, #9426, #3445 ) ) ;
#9641=DIRECTION ( 'NONE',  ( 1.000000000000000000, 0.000000000000000000, -0.000000000000000000 ) ) ;
#9657=ORIENTED_EDGE ( 'NONE', *, *, #12501, .T. ) ;
#9658=ORIENTED_EDGE ( 'NONE', *, *, #825, .F. ) ;
#9661=ORIENTED_EDGE ( 'NONE', *, *, #19128, .T. ) ;
#9663=EDGE_CURVE ( 'NONE', #20330, #445, #17494, .T. ) ;
#9688=AXIS2_PLACEMENT_3D ( 'NONE', #789, #7634, #11084 ) ;
#9691=DIRECTION ( 'NONE',  ( 0.000000000000000000, 0.000000000000000000, -1.000000000000000000 ) ) ;
#9710=ORIENTED_EDGE ( 'NONE', *, *, #15865, .T. ) ;
#9727=CARTESIAN_POINT ( 'NONE',  ( 34.69999999999999574, 85.00000000000000000, 3.009745230819759520E-15 ) ) ;
#9739=EDGE_CURVE ( 'NONE', #20557, #3842, #10376, .T. ) ;
#9740=ORIENTED_EDGE ( 'NONE', *, *, #5153, .F. ) ;
#9742=CIRCLE ( 'NONE', #4022, 0.2999999999999999334 ) ;
#9760=DIRECTION ( 'NONE',  ( 0.000000000000000000, 0.000000000000000000, -1.000000000000000000 ) ) ;
#9767=CARTESIAN_POINT ( 'NONE',  ( 0.000000000000000000, 0.000000000000000000, 0.000000000000000000 ) ) ;
#9786=CARTESIAN_POINT ( 'NONE',  ( 33.19999999999999574, 85.00000000000000000, 1.799999999999996048 ) ) ;
#9796=CARTESIAN_POINT ( 'NONE',  ( -34.70000000000000284, -85.00000000000000000, 0.6000000000000033085 ) ) ;
#9799=DIRECTION ( 'NONE',  ( -0.000000000000000000, 1.000000000000000000, -0.000000000000000000 ) ) ;
#9809=CARTESIAN_POINT ( 'NONE',  ( -33.20000000000000284, -84.70000000000001705, 1.800000000000000266 ) ) ;
#9831=DIRECTION ( 'NONE',  ( 1.000000000000000000, -0.000000000000000000, 6.123233995736764803E-17 ) ) ;
#9839=DIRECTION ( 'NONE',  ( -1.000000000000000000, 0.000000000000000000, 0.000000000000000000 ) ) ;
#9853=VECTOR ( 'NONE', #7558, 1000.000000000000000 ) ;
#9873=VECTOR ( 'NONE', #6902, 1000.000000000000000 ) ;
#9891=VERTEX_POINT ( 'NONE', #10009 ) ;
#9911=EDGE_LOOP ( 'NONE', ( #11836, #21876, #7852, #4407 ) ) ;
#9914=CARTESIAN_POINT ( 'NONE',  ( -34.39999999999999858, 85.00000000000000000, 3.673940397442079220E-17 ) ) ;
#9916=ORIENTED_EDGE ( 'NONE', *, *, #15757, .F. ) ;
#9937=FACE_OUTER_BOUND ( 'NONE', #16954, .T. ) ;
#9944=DIRECTION ( 'NONE',  ( -1.000000000000000000, 0.000000000000000000, -6.123233995736764803E-17 ) ) ;
#9945=DIRECTION ( 'NONE',  ( 0.000000000000000000, -1.000000000000000000, 0.000000000000000000 ) ) ;
#9967=EDGE_CURVE ( 'NONE', #8145, #9143, #659, .T. ) ;
#9988=CIRCLE ( 'NONE', #3197, 0.6000000000000000888 ) ;
#9992=LINE ( 'NONE', #1474, #20952 ) ;
#9996=VERTEX_POINT ( 'NONE', #15035 ) ;
#10008=DIRECTION ( 'NONE',  ( -6.123233995736766036E-17, 0.000000000000000000, 1.000000000000000000 ) ) ;
#10009=CARTESIAN_POINT ( 'NONE',  ( -35.00000000000000000, -84.70000000000001705, 0.6000000000000033085 ) ) ;
#10015=TOROIDAL_SURFACE ( 'NONE', #17515, 0.2999999999999999889, 0.2999999999999999889 ) ;
#10021=CARTESIAN_POINT ( 'NONE',  ( -30.49999999999999289, -123.9599366953518711, 9.999999999999998224 ) ) ;
#10027=CARTESIAN_POINT ( 'NONE',  ( -30.19999999999999574, 69.70000000000001705, 1.199999999999999734 ) ) ;
#10031=AXIS2_PLACEMENT_3D ( 'NONE', #9513, #2470, #882 ) ;
#10063=VECTOR ( 'NONE', #815, 1000.000000000000000 ) ;
#10066=EDGE_CURVE ( 'NONE', #12623, #15917, #2036, .T. ) ;
#10080=FACE_OUTER_BOUND ( 'NONE', #4331, .T. ) ;
#10086=DIRECTION ( 'NONE',  ( 0.000000000000000000, 0.000000000000000000, -1.000000000000000000 ) ) ;
#10091=EDGE_CURVE ( 'NONE', #2915, #10170, #9091, .T. ) ;
#10101=ORIENTED_EDGE ( 'NONE', *, *, #13681, .F. ) ;
#10120=EDGE_CURVE ( 'NONE', #675, #3754, #7105, .T. ) ;
#10124=VERTEX_POINT ( 'NONE', #13778 ) ;
#10132=SURFACE_SIDE_STYLE ('',( #8344 ) ) ;
#10140=ORIENTED_EDGE ( 'NONE', *, *, #18082, .T. ) ;
#10141=ORIENTED_EDGE ( 'NONE', *, *, #20490, .F. ) ;
#10170=VERTEX_POINT ( 'NONE', #20637 ) ;
#10178=CARTESIAN_POINT ( 'NONE',  ( 30.49999999999999645, 69.70000000000000284, 1.753093177964017524E-15 ) ) ;
#10182=CARTESIAN_POINT ( 'NONE',  ( 34.99999999999999289, -84.70000000000001705, 0.6000000000000033085 ) ) ;
#10209=VERTEX_POINT ( 'NONE', #16347 ) ;
#10211=ADVANCED_FACE ( 'NONE', ( #20338 ), #9207, .T. ) ;
#10257=ORIENTED_EDGE ( 'NONE', *, *, #2918, .T. ) ;
#10281=FACE_OUTER_BOUND ( 'NONE', #595, .T. ) ;
#10286=ORIENTED_EDGE ( 'NONE', *, *, #13316, .T. ) ;
#10326=ORIENTED_EDGE ( 'NONE', *, *, #3915, .F. ) ;
#10336=CARTESIAN_POINT ( 'NONE',  ( -34.40000000000001279, 85.00000000000000000, 79.69999999999998863 ) ) ;
#10344=ORIENTED_EDGE ( 'NONE', *, *, #5003, .T. ) ;
#10376=LINE ( 'NONE', #17184, #4086 ) ;
#10381=ORIENTED_EDGE ( 'NONE', *, *, #21406, .F. ) ;
#10406=EDGE_CURVE ( 'NONE', #6840, #8641, #13829, .T. ) ;
#10426=EDGE_LOOP ( 'NONE', ( #2796, #16122, #5937, #20184 ) ) ;
#10431=VERTEX_POINT ( 'NONE', #20883 ) ;
#10466=DIRECTION ( 'NONE',  ( 0.000000000000000000, 0.000000000000000000, -1.000000000000000000 ) ) ;
#10476=CARTESIAN_POINT ( 'NONE',  ( -30.79999999999999361, -84.70000000000001705, 0.3000000000000002665 ) ) ;
#10483=CARTESIAN_POINT ( 'NONE',  ( 0.000000000000000000, 85.00000000000000000, 0.000000000000000000 ) ) ;
#10488=DIRECTION ( 'NONE',  ( -8.673617379884034239E-17, 0.000000000000000000, 1.000000000000000000 ) ) ;
#10492=ADVANCED_FACE ( 'NONE', ( #19986 ), #8503, .T. ) ;
#10511=CIRCLE ( 'NONE', #20882, 0.2999999999999999889 ) ;
#10523=CARTESIAN_POINT ( 'NONE',  ( 34.39999999999998437, 84.70000000000001705, 0.3000000000000042077 ) ) ;
#10530=ORIENTED_EDGE ( 'NONE', *, *, #17726, .T. ) ;
#10540=DIRECTION ( 'NONE',  ( -1.000000000000000000, 0.000000000000000000, -8.673617379883930701E-17 ) ) ;
#10541=ADVANCED_FACE ( 'NONE', ( #7786 ), #19637, .F. ) ;
#10549=CARTESIAN_POINT ( 'NONE',  ( -33.50000000000000000, 85.00000000000000000, 1.800000000000000266 ) ) ;
#10556=AXIS2_PLACEMENT_3D ( 'NONE', #20543, #11476, #2979 ) ;
#10594=DIRECTION ( 'NONE',  ( 0.000000000000000000, 1.000000000000000000, 0.000000000000000000 ) ) ;
#10598=DIRECTION ( 'NONE',  ( -8.673617379884034239E-17, 0.000000000000000000, 1.000000000000000000 ) ) ;
#10601=AXIS2_PLACEMENT_3D ( 'NONE', #20006, #21903, #4882 ) ;
#10602=PLANE ( 'NONE',  #18401 ) ;
#10609=ORIENTED_EDGE ( 'NONE', *, *, #1298, .F. ) ;
#10617=VECTOR ( 'NONE', #2661, 1000.000000000000000 ) ;
#10623=EDGE_CURVE ( 'NONE', #3486, #19413, #13770, .T. ) ;
#10637=CIRCLE ( 'NONE', #4922, 0.3000000000000016542 ) ;
#10655=AXIS2_PLACEMENT_3D ( 'NONE', #15174, #6823, #17406 ) ;
#10669=ORIENTED_EDGE ( 'NONE', *, *, #16599, .F. ) ;
#10709=DIRECTION ( 'NONE',  ( 0.000000000000000000, 0.000000000000000000, 1.000000000000000000 ) ) ;
#10721=AXIS2_PLACEMENT_3D ( 'NONE', #3439, #8155, #1305 ) ;
#10740=CARTESIAN_POINT ( 'NONE',  ( 34.39999999999998437, -84.70000000000001705, 0.6000000000000041966 ) ) ;
#10753=ADVANCED_FACE ( 'NONE', ( #20361 ), #16872, .T. ) ;
#10756=ORIENTED_EDGE ( 'NONE', *, *, #6493, .T. ) ;
#10757=EDGE_CURVE ( 'NONE', #6609, #7001, #1775, .T. ) ;
#10763=CYLINDRICAL_SURFACE ( 'NONE', #5204, 0.3000000000000016542 ) ;
#10765=VECTOR ( 'NONE', #13040, 1000.000000000000000 ) ;
#10785=DIRECTION ( 'NONE',  ( 1.000000000000000000, 0.000000000000000000, 0.000000000000000000 ) ) ;
#10787=CARTESIAN_POINT ( 'NONE',  ( -33.50000000000000000, 84.70000000000001705, 1.800000000000000266 ) ) ;
#10799=CARTESIAN_POINT ( 'NONE',  ( 30.79999999999999361, 85.00000000000000000, 4.029087969194791265E-15 ) ) ;
#10802=ORIENTED_EDGE ( 'NONE', *, *, #5124, .F. ) ;
#10804=DIRECTION ( 'NONE',  ( 1.000000000000000000, 0.000000000000000000, 0.000000000000000000 ) ) ;
#10819=FACE_OUTER_BOUND ( 'NONE', #14264, .T. ) ;
#10823=DIRECTION ( 'NONE',  ( -6.123233995736764803E-17, 0.000000000000000000, 1.000000000000000000 ) ) ;
#10842=EDGE_CURVE ( 'NONE', #823, #20557, #17723, .T. ) ;
#10846=DIRECTION ( 'NONE',  ( -6.123233995736764803E-17, 0.000000000000000000, 1.000000000000000000 ) ) ;
#10861=VECTOR ( 'NONE', #181, 1000.000000000000000 ) ;
#10863=DIRECTION ( 'NONE',  ( 0.000000000000000000, -1.000000000000000000, 0.000000000000000000 ) ) ;
#10882=DIRECTION ( 'NONE',  ( 0.000000000000000000, 0.000000000000000000, 1.000000000000000000 ) ) ;
#10885=CARTESIAN_POINT ( 'NONE',  ( -34.39999999999999858, 84.70000000000001705, 3.673940397442079220E-17 ) ) ;
#10888=ADVANCED_FACE ( 'NONE', ( #15739 ), #20591, .T. ) ;
#10892=EDGE_CURVE ( 'NONE', #21431, #13921, #19226, .T. ) ;
#10893=CARTESIAN_POINT ( 'NONE',  ( 30.79999999999999716, -84.70000000000001705, 4.029087969194791265E-15 ) ) ;
#10916=AXIS2_PLACEMENT_3D ( 'NONE', #20565, #20227, #12039 ) ;
#10922=ORIENTED_EDGE ( 'NONE', *, *, #11896, .F. ) ;
#10929=AXIS2_PLACEMENT_3D ( 'NONE', #13464, #21985, #18616 ) ;
#10930=ORIENTED_EDGE ( 'NONE', *, *, #6370, .T. ) ;
#10935=ADVANCED_FACE ( 'NONE', ( #13950 ), #9141, .T. ) ;
#10936=EDGE_LOOP ( 'NONE', ( #2832, #848, #15138, #13791 ) ) ;
#10940=DIRECTION ( 'NONE',  ( -0.000000000000000000, 1.000000000000000000, -0.000000000000000000 ) ) ;
#10959=CIRCLE ( 'NONE', #10556, 0.2999999999999947153 ) ;
#10979=CARTESIAN_POINT ( 'NONE',  ( -35.00000000000000000, -84.70000000000001705, 1.500000000000000000 ) ) ;
#10984=ORIENTED_EDGE ( 'NONE', *, *, #12501, .F. ) ;
#10999=VERTEX_POINT ( 'NONE', #14613 ) ;
#11004=CIRCLE ( 'NONE', #6012, 0.3000000000000016542 ) ;
#11012=ORIENTED_EDGE ( 'NONE', *, *, #18082, .F. ) ;
#11013=ORIENTED_EDGE ( 'NONE', *, *, #20692, .F. ) ;
#11023=VECTOR ( 'NONE', #21255, 1000.000000000000000 ) ;
#11026=LINE ( 'NONE', #13934, #12413 ) ;
#11046=EDGE_CURVE ( 'NONE', #12088, #9996, #14826, .T. ) ;
#11049=VERTEX_POINT ( 'NONE', #17970 ) ;
#11053=EDGE_LOOP ( 'NONE', ( #6435, #2860, #18953, #20206 ) ) ;
#11066=EDGE_CURVE ( 'NONE', #5502, #12260, #6685, .T. ) ;
#11067=CARTESIAN_POINT ( 'NONE',  ( 33.49999999999998579, -84.70000000000001705, 80.00000000000000000 ) ) ;
#11071=VERTEX_POINT ( 'NONE', #14386 ) ;
#11075=ORIENTED_EDGE ( 'NONE', *, *, #10757, .T. ) ;
#11079=CARTESIAN_POINT ( 'NONE',  ( -33.80000000000001847, -84.70000000000001705, 78.20000000000000284 ) ) ;
#11082=DIRECTION ( 'NONE',  ( 0.000000000000000000, 0.000000000000000000, -1.000000000000000000 ) ) ;
#11084=DIRECTION ( 'NONE',  ( 0.000000000000000000, 0.000000000000000000, -1.000000000000000000 ) ) ;
#11096=FILL_AREA_STYLE ('',( #21294 ) ) ;
#11104=AXIS2_PLACEMENT_3D ( 'NONE', #14851, #12015, #18864 ) ;
#11115=ORIENTED_EDGE ( 'NONE', *, *, #14595, .F. ) ;
#11122=CARTESIAN_POINT ( 'NONE',  ( 34.39999999999998437, -84.70000000000001705, 79.39999999999999147 ) ) ;
#11126=CARTESIAN_POINT ( 'NONE',  ( 30.79999999999999716, -84.70000000000001705, 1.200000000000004174 ) ) ;
#11143=ORIENTED_EDGE ( 'NONE', *, *, #6782, .F. ) ;
#11144=DIRECTION ( 'NONE',  ( 0.000000000000000000, 0.000000000000000000, -1.000000000000000000 ) ) ;
#11147=ORIENTED_EDGE ( 'NONE', *, *, #15366, .F. ) ;
#11161=DIRECTION ( 'NONE',  ( -6.123233995736764803E-17, 0.000000000000000000, 1.000000000000000000 ) ) ;
#11185=ADVANCED_FACE ( 'NONE', ( #11576 ), #2006, .T. ) ;
#11219=DIRECTION ( 'NONE',  ( 1.734723475976806848E-16, -0.000000000000000000, -1.000000000000000000 ) ) ;
#11235=CARTESIAN_POINT ( 'NONE',  ( -30.79999999999999361, -84.70000000000001705, 1.200000000000000400 ) ) ;
#11252=EDGE_CURVE ( 'NONE', #3127, #12578, #21697, .T. ) ;
#11280=CARTESIAN_POINT ( 'NONE',  ( -33.80000000000000426, 84.70000000000001705, 1.800000000000000266 ) ) ;
#11301=AXIS2_PLACEMENT_3D ( 'NONE', #12690, #6029, #740 ) ;
#11305=DIRECTION ( 'NONE',  ( 1.000000000000000000, 0.000000000000000000, 1.734723475976786140E-16 ) ) ;
#11334=EDGE_LOOP ( 'NONE', ( #2012, #19551, #8208, #4672 ) ) ;
#11337=EDGE_LOOP ( 'NONE', ( #14693, #993, #5247, #7587 ) ) ;
#11344=EDGE_CURVE ( 'NONE', #14491, #14946, #271, .T. ) ;
#11357=ORIENTED_EDGE ( 'NONE', *, *, #18292, .T. ) ;
#11359=FACE_OUTER_BOUND ( 'NONE', #10936, .T. ) ;
#11373=ORIENTED_EDGE ( 'NONE', *, *, #19642, .F. ) ;
#11409=CYLINDRICAL_SURFACE ( 'NONE', #17927, 0.2999999999999947153 ) ;
#11418=CYLINDRICAL_SURFACE ( 'NONE', #17240, 0.3000000000000016542 ) ;
#11430=ORIENTED_EDGE ( 'NONE', *, *, #19963, .T. ) ;
#11443=ORIENTED_EDGE ( 'NONE', *, *, #6815, .F. ) ;
#11446=DIRECTION ( 'NONE',  ( 1.734723475976806848E-16, -0.000000000000000000, -1.000000000000000000 ) ) ;
#11449=EDGE_LOOP ( 'NONE', ( #10802, #10669, #18624, #13032 ) ) ;
#11451=ORIENTED_EDGE ( 'NONE', *, *, #18615, .T. ) ;
#11475=DIRECTION ( 'NONE',  ( 0.000000000000000000, -1.000000000000000000, 0.000000000000000000 ) ) ;
#11476=DIRECTION ( 'NONE',  ( 1.000000000000000000, 0.000000000000000000, 0.000000000000000000 ) ) ;
#11482=EDGE_LOOP ( 'NONE', ( #464, #10922, #14350, #10984 ) ) ;
#11487=ORIENTED_EDGE ( 'NONE', *, *, #1298, .T. ) ;
#11495=CARTESIAN_POINT ( 'NONE',  ( 33.19999999999999574, 84.70000000000001705, 1.200000000000004174 ) ) ;
#11519=DIRECTION ( 'NONE',  ( 0.000000000000000000, -1.000000000000000000, 0.000000000000000000 ) ) ;
#11530=FACE_OUTER_BOUND ( 'NONE', #10426, .T. ) ;
#11531=ORIENTED_EDGE ( 'NONE', *, *, #7720, .F. ) ;
#11566=DIRECTION ( 'NONE',  ( 0.000000000000000000, 0.000000000000000000, 1.000000000000000000 ) ) ;
#11570=DIRECTION ( 'NONE',  ( 0.000000000000000000, 1.000000000000000000, 0.000000000000000000 ) ) ;
#11576=FACE_OUTER_BOUND ( 'NONE', #2532, .T. ) ;
#11581=DIRECTION ( 'NONE',  ( 1.000000000000000000, 0.000000000000000000, 0.000000000000000000 ) ) ;
#11587=DIRECTION ( 'NONE',  ( 0.000000000000000000, 0.000000000000000000, -1.000000000000000000 ) ) ;
#11597=CARTESIAN_POINT ( 'NONE',  ( -30.79999999999999361, -84.70000000000001705, 0.2999999999999999334 ) ) ;
#11599=ORIENTED_EDGE ( 'NONE', *, *, #3561, .F. ) ;
#11600=LINE ( 'NONE', #16870, #20564 ) ;
#11608=DIRECTION ( 'NONE',  ( -6.123233995736764803E-17, 0.000000000000000000, 1.000000000000000000 ) ) ;
#11614=DIRECTION ( 'NONE',  ( 8.673617379884034239E-17, 0.000000000000000000, -1.000000000000000000 ) ) ;
#11616=CARTESIAN_POINT ( 'NONE',  ( 33.79999999999999716, 85.00000000000000000, 1.799999999999996048 ) ) ;
#11628=ORIENTED_EDGE ( 'NONE', *, *, #11896, .T. ) ;
#11667=CIRCLE ( 'NONE', #951, 0.3000000000000000444 ) ;
#11668=AXIS2_PLACEMENT_3D ( 'NONE', #15192, #11608, #18445 ) ;
#11674=EDGE_CURVE ( 'NONE', #5502, #17668, #3932, .T. ) ;
#11682=AXIS2_PLACEMENT_3D ( 'NONE', #15778, #3948, #9187 ) ;
#11684=DIRECTION ( 'NONE',  ( -6.123233995736764803E-17, 0.000000000000000000, 1.000000000000000000 ) ) ;
#11700=EDGE_CURVE ( 'NONE', #9461, #5502, #3849, .T. ) ;
#11710=AXIS2_PLACEMENT_3D ( 'NONE', #6502, #6719, #13298 ) ;
#11713=FACE_OUTER_BOUND ( 'NONE', #21754, .T. ) ;
#11719=DIRECTION ( 'NONE',  ( 0.000000000000000000, 0.000000000000000000, -1.000000000000000000 ) ) ;
#11726=ORIENTED_EDGE ( 'NONE', *, *, #17035, .T. ) ;
#11730=AXIS2_PLACEMENT_3D ( 'NONE', #2868, #16160, #6017 ) ;
#11738=ORIENTED_EDGE ( 'NONE', *, *, #10406, .F. ) ;
#11747=DIRECTION ( 'NONE',  ( 0.000000000000000000, -1.000000000000000000, 0.000000000000000000 ) ) ;
#11759=ORIENTED_EDGE ( 'NONE', *, *, #11988, .T. ) ;
#11769=EDGE_CURVE ( 'NONE', #341, #10170, #15610, .T. ) ;
#11779=DIRECTION ( 'NONE',  ( 1.734723475976806848E-16, -0.000000000000000000, -1.000000000000000000 ) ) ;
#11799=AXIS2_PLACEMENT_3D ( 'NONE', #17143, #15462, #131 ) ;
#11812=DIRECTION ( 'NONE',  ( 0.000000000000000000, -1.000000000000000000, 3.614007241618411485E-15 ) ) ;
#11836=ORIENTED_EDGE ( 'NONE', *, *, #16599, .T. ) ;
#11877=EDGE_CURVE ( 'NONE', #5205, #8641, #1336, .T. ) ;
#11893=EDGE_CURVE ( 'NONE', #14859, #15917, #2040, .T. ) ;
#11896=EDGE_CURVE ( 'NONE', #21952, #6609, #7718, .T. ) ;
#11908=FACE_OUTER_BOUND ( 'NONE', #11334, .T. ) ;
#11914=ORIENTED_EDGE ( 'NONE', *, *, #865, .F. ) ;
#11916=DIRECTION ( 'NONE',  ( 0.000000000000000000, 0.000000000000000000, -1.000000000000000000 ) ) ;
#11919=ORIENTED_EDGE ( 'NONE', *, *, #5153, .T. ) ;
#11942=LINE ( 'NONE', #17107, #21401 ) ;
#11944=ORIENTED_EDGE ( 'NONE', *, *, #14108, .F. ) ;
#11953=DIRECTION ( 'NONE',  ( 0.000000000000000000, -1.000000000000000000, 0.000000000000000000 ) ) ;
#11973=EDGE_CURVE ( 'NONE', #1975, #8082, #15630, .T. ) ;
#11988=EDGE_CURVE ( 'NONE', #13680, #21291, #11004, .T. ) ;
#11996=DIRECTION ( 'NONE',  ( -0.000000000000000000, 1.000000000000000000, -0.000000000000000000 ) ) ;
#12000=DIRECTION ( 'NONE',  ( 0.000000000000000000, 0.000000000000000000, -1.000000000000000000 ) ) ;
#12002=CARTESIAN_POINT ( 'NONE',  ( -30.79999999999999005, 69.70000000000001705, 2.571758278209448859E-16 ) ) ;
#12006=EDGE_LOOP ( 'NONE', ( #1065, #6903, #19373, #20271, #20313, #19666, #2206, #6543 ) ) ;
#12011=DIRECTION ( 'NONE',  ( -0.000000000000000000, 1.000000000000000000, -0.000000000000000000 ) ) ;
#12015=DIRECTION ( 'NONE',  ( -6.123233995736764803E-17, 0.000000000000000000, 1.000000000000000000 ) ) ;
#12036=AXIS2_PLACEMENT_3D ( 'NONE', #14764, #13200, #14651 ) ;
#12039=DIRECTION ( 'NONE',  ( 0.000000000000000000, 0.000000000000000000, 1.000000000000000000 ) ) ;
#12057=LINE ( 'NONE', #6947, #18478 ) ;
#12059=AXIS2_PLACEMENT_3D ( 'NONE', #16039, #7342, #2185 ) ;
#12061=AXIS2_PLACEMENT_3D ( 'NONE', #1489, #15135, #6778 ) ;
#12066=CARTESIAN_POINT ( 'NONE',  ( -34.39999999999999858, -84.70000000000001705, 3.673940397442079220E-17 ) ) ;
#12069=CARTESIAN_POINT ( 'NONE',  ( -30.49999999999999289, -84.70000000000001705, 0.2999999999999999334 ) ) ;
#12082=ORIENTED_EDGE ( 'NONE', *, *, #8567, .T. ) ;
#12088=VERTEX_POINT ( 'NONE', #2214 ) ;
#12116=FACE_OUTER_BOUND ( 'NONE', #18332, .T. ) ;
#12133=ORIENTED_EDGE ( 'NONE', *, *, #15510, .T. ) ;
#12150=AXIS2_PLACEMENT_3D ( 'NONE', #11079, #19468, #7405 ) ;
#12161=ORIENTED_EDGE ( 'NONE', *, *, #16057, .T. ) ;
#12163=ORIENTED_EDGE ( 'NONE', *, *, #12800, .T. ) ;
#12167=ORIENTED_EDGE ( 'NONE', *, *, #13334, .F. ) ;
#12170=CARTESIAN_POINT ( 'NONE',  ( 34.39999999999998437, 84.70000000000001705, 80.00000000000000000 ) ) ;
#12177=DIRECTION ( 'NONE',  ( -2.891205793294662845E-15, -0.000000000000000000, -1.000000000000000000 ) ) ;
#12185=DIRECTION ( 'NONE',  ( 0.000000000000000000, 0.000000000000000000, 1.000000000000000000 ) ) ;
#12205=CARTESIAN_POINT ( 'NONE',  ( -30.19999999999999574, 70.29999999999999716, 1.500000000000000222 ) ) ;
#12225=DIRECTION ( 'NONE',  ( 1.000000000000000000, 0.000000000000000000, 6.123233995736764803E-17 ) ) ;
#12244=ORIENTED_EDGE ( 'NONE', *, *, #10892, .T. ) ;
#12260=VERTEX_POINT ( 'NONE', #8032 ) ;
#12280=VERTEX_POINT ( 'NONE', #1083 ) ;
#12302=DIRECTION ( 'NONE',  ( 0.000000000000000000, 0.000000000000000000, 1.000000000000000000 ) ) ;
#12324=DIRECTION ( 'NONE',  ( 0.000000000000000000, 1.000000000000000000, 0.000000000000000000 ) ) ;
#12334=DIRECTION ( 'NONE',  ( -0.000000000000000000, 1.000000000000000000, -0.000000000000000000 ) ) ;
#12349=EDGE_CURVE ( 'NONE', #10209, #9996, #15313, .T. ) ;
#12360=ORIENTED_EDGE ( 'NONE', *, *, #20692, .T. ) ;
#12367=ORIENTED_EDGE ( 'NONE', *, *, #21569, .T. ) ;
#12413=VECTOR ( 'NONE', #5892, 1000.000000000000000 ) ;
#12463=VERTEX_POINT ( 'NONE', #20170 ) ;
#12478=ORIENTED_EDGE ( 'NONE', *, *, #18176, .F. ) ;
#12501=EDGE_CURVE ( 'NONE', #17830, #7599, #19683, .T. ) ;
#12509=DIRECTION ( 'NONE',  ( 1.000000000000000000, 0.000000000000000000, -2.891205793294662451E-15 ) ) ;
#12532=CARTESIAN_POINT ( 'NONE',  ( 30.49999999999999645, 70.29999999999999716, 0.3000000000000033751 ) ) ;
#12542=EDGE_CURVE ( 'NONE', #6971, #9271, #17350, .T. ) ;
#12565=CARTESIAN_POINT ( 'NONE',  ( -30.79999999999999005, 70.00000000000001421, 1.500000000000000222 ) ) ;
#12566=APPLICATION_CONTEXT ( 'automotive_design' ) ;
#12578=VERTEX_POINT ( 'NONE', #6160 ) ;
#12590=CARTESIAN_POINT ( 'NONE',  ( -35.00000000000000000, 85.00000000000000000, 0.000000000000000000 ) ) ;
#12623=VERTEX_POINT ( 'NONE', #19793 ) ;
#12626=DIRECTION ( 'NONE',  ( 0.000000000000000000, -1.000000000000000000, 0.000000000000000000 ) ) ;
#12637=VECTOR ( 'NONE', #21895, 1000.000000000000000 ) ;
#12640=ADVANCED_FACE ( 'NONE', ( #4456 ), #18327, .F. ) ;
#12649=DIRECTION ( 'NONE',  ( -0.000000000000000000, 1.000000000000000000, -0.000000000000000000 ) ) ;
#12673=DIRECTION ( 'NONE',  ( 0.000000000000000000, 0.000000000000000000, 1.000000000000000000 ) ) ;
#12683=DIRECTION ( 'NONE',  ( -1.734723475976806848E-16, 0.000000000000000000, 1.000000000000000000 ) ) ;
#12690=CARTESIAN_POINT ( 'NONE',  ( 34.39999999999998437, 84.70000000000001705, 0.6000000000000041966 ) ) ;
#12700=CIRCLE ( 'NONE', #15565, 0.5999999999999998668 ) ;
#12704=ORIENTED_EDGE ( 'NONE', *, *, #1073, .F. ) ;
#12718=CARTESIAN_POINT ( 'NONE',  ( 34.39999999999998437, 85.00000000000000000, 0.6000000000000041966 ) ) ;
#12729=ADVANCED_FACE ( 'NONE', ( #5134 ), #8610, .T. ) ;
#12735=DIRECTION ( 'NONE',  ( 1.000000000000000000, -0.000000000000000000, 0.000000000000000000 ) ) ;
#12748=CARTESIAN_POINT ( 'NONE',  ( -33.80000000000001847, 85.00000000000000000, 78.20000000000000284 ) ) ;
#12756=CYLINDRICAL_SURFACE ( 'NONE', #15299, 0.2999999999999999334 ) ;
#12768=EDGE_CURVE ( 'NONE', #5602, #12260, #13183, .T. ) ;
#12774=ADVANCED_FACE ( 'NONE', ( #6832 ), #14971, .T. ) ;
#12796=DIRECTION ( 'NONE',  ( 0.000000000000000000, 0.000000000000000000, -1.000000000000000000 ) ) ;
#12797=AXIS2_PLACEMENT_3D ( 'NONE', #17100, #13513, #92 ) ;
#12800=EDGE_CURVE ( 'NONE', #14491, #10431, #6771, .T. ) ;
#12802=DIRECTION ( 'NONE',  ( 1.734723475976806848E-16, -0.000000000000000000, -1.000000000000000000 ) ) ;
#12810=ORIENTED_EDGE ( 'NONE', *, *, #21406, .T. ) ;
#12815=ORIENTED_EDGE ( 'NONE', *, *, #8795, .T. ) ;
#12818=DIRECTION ( 'NONE',  ( 0.000000000000000000, -1.000000000000000000, 0.000000000000000000 ) ) ;
#12822=ADVANCED_FACE ( 'NONE', ( #10281 ), #5474, .T. ) ;
#12825=CARTESIAN_POINT ( 'NONE',  ( 34.39999999999998437, -85.00000000000000000, 79.69999999999998863 ) ) ;
#12846=CIRCLE ( 'NONE', #5376, 0.2999999999999999334 ) ;
#12850=SHAPE_REPRESENTATION ( 'Lampshade', ( #17493 ), #5511 ) ;
#12874=( LENGTH_UNIT ( ) NAMED_UNIT ( * ) SI_UNIT ( .MILLI., .METRE. ) );
#12885=( GEOMETRIC_REPRESENTATION_CONTEXT ( 3 ) GLOBAL_UNCERTAINTY_ASSIGNED_CONTEXT ( ( #6425 ) ) GLOBAL_UNIT_ASSIGNED_CONTEXT ( ( #8577, #13479, #13915 ) ) REPRESENTATION_CONTEXT ( 'NONE', 'WORKASPACE' ) );
#12902=AXIS2_PLACEMENT_3D ( 'NONE', #17819, #5438, #12225 ) ;
#12915=ORIENTED_EDGE ( 'NONE', *, *, #6092, .T. ) ;
#12934=ORIENTED_EDGE ( 'NONE', *, *, #16107, .T. ) ;
#12944=CARTESIAN_POINT ( 'NONE',  ( -35.00000000000001421, -84.70000000000001705, 79.70000000000000284 ) ) ;
#12947=ORIENTED_EDGE ( 'NONE', *, *, #7630, .T. ) ;
#12954=ORIENTED_EDGE ( 'NONE', *, *, #15664, .F. ) ;
#12956=CARTESIAN_POINT ( 'NONE',  ( -33.20000000000000284, -84.70000000000001705, 1.200000000000000400 ) ) ;
#12958=EDGE_CURVE ( 'NONE', #19724, #1963, #17556, .T. ) ;
#12960=ORIENTED_EDGE ( 'NONE', *, *, #11066, .F. ) ;
#12961=FACE_OUTER_BOUND ( 'NONE', #3605, .T. ) ;
#12970=CARTESIAN_POINT ( 'NONE',  ( -34.39999999999999858, 85.00000000000000000, 0.6000000000000033085 ) ) ;
#12971=SPHERICAL_SURFACE ( 'NONE', #6174, 0.2999999999999999889 ) ;
#12979=DIRECTION ( 'NONE',  ( 1.000000000000000000, -0.000000000000000000, 6.123233995736764803E-17 ) ) ;
#12988=LINE ( 'NONE', #18031, #17710 ) ;
#13025=VECTOR ( 'NONE', #9041, 1000.000000000000000 ) ;
#13032=ORIENTED_EDGE ( 'NONE', *, *, #11877, .F. ) ;
#13040=DIRECTION ( 'NONE',  ( 0.000000000000000000, -1.000000000000000000, 0.000000000000000000 ) ) ;
#13045=DIRECTION ( 'NONE',  ( -8.673617379884034239E-17, 0.000000000000000000, 1.000000000000000000 ) ) ;
#13046=CARTESIAN_POINT ( 'NONE',  ( -34.40000000000001279, 84.70000000000001705, 80.00000000000000000 ) ) ;
#13072=VECTOR ( 'NONE', #7735, 1000.000000000000000 ) ;
#13075=DIRECTION ( 'NONE',  ( 1.734723475976806848E-16, 0.000000000000000000, -1.000000000000000000 ) ) ;
#13083=CARTESIAN_POINT ( 'NONE',  ( -30.49999999999998934, 70.00000000000000000, 1.199999999999999512 ) ) ;
#13086=DIRECTION ( 'NONE',  ( 1.000000000000000000, 0.000000000000000000, 0.000000000000000000 ) ) ;
#13110=VECTOR ( 'NONE', #17155, 1000.000000000000000 ) ;
#13111=ADVANCED_BREP_SHAPE_REPRESENTATION ( '', ( #13188, #17493 ), #5511 ) ;
#13123=VECTOR ( 'NONE', #1958, 1000.000000000000000 ) ;
#13133=AXIS2_PLACEMENT_3D ( 'NONE', #6892, #4854, #10008 ) ;
#13150=CARTESIAN_POINT ( 'NONE',  ( -30.19999999999999574, 69.70000000000001705, 2.710505431213761085E-16 ) ) ;
#13155=CARTESIAN_POINT ( 'NONE',  ( 30.79999999999999716, -123.9599366953518711, 0.3000000000000033751 ) ) ;
#13157=EDGE_CURVE ( 'NONE', #4505, #814, #18674, .T. ) ;
#13158=ORIENTED_EDGE ( 'NONE', *, *, #15366, .T. ) ;
#13176=DIRECTION ( 'NONE',  ( 0.000000000000000000, 0.000000000000000000, -1.000000000000000000 ) ) ;
#13183=CIRCLE ( 'NONE', #14239, 0.3000000000000016542 ) ;
#13188=MANIFOLD_SOLID_BREP ( 'Stock-MAS-696-1', #1321 ) ;
#13200=DIRECTION ( 'NONE',  ( -6.123233995736764803E-17, 0.000000000000000000, 1.000000000000000000 ) ) ;
#13256=AXIS2_PLACEMENT_3D ( 'NONE', #1338, #8295, #18347 ) ;
#13271=CARTESIAN_POINT ( 'NONE',  ( 30.79999999999999716, -84.70000000000001705, 1.500000000000004219 ) ) ;
#13279=DIRECTION ( 'NONE',  ( 0.000000000000000000, 0.000000000000000000, -1.000000000000000000 ) ) ;
#13282=CIRCLE ( 'NONE', #15074, 0.2999999999999999334 ) ;
#13284=DIRECTION ( 'NONE',  ( 0.000000000000000000, 0.000000000000000000, -1.000000000000000000 ) ) ;
#13289=AXIS2_PLACEMENT_3D ( 'NONE', #14002, #14100, #7205 ) ;
#13290=CARTESIAN_POINT ( 'NONE',  ( -35.00000000000000000, 85.00000000000000000, 0.6000000000000033085 ) ) ;
#13298=DIRECTION ( 'NONE',  ( 0.000000000000000000, 0.000000000000000000, -1.000000000000000000 ) ) ;
#13300=ORIENTED_EDGE ( 'NONE', *, *, #1491, .F. ) ;
#13302=AXIS2_PLACEMENT_3D ( 'NONE', #18228, #7616, #21159 ) ;
#13304=ADVANCED_FACE ( 'NONE', ( #7553 ), #3976, .F. ) ;
#13316=EDGE_CURVE ( 'NONE', #12280, #8060, #20450, .T. ) ;
#13318=LINE ( 'NONE', #8397, #15867 ) ;
#13328=VERTEX_POINT ( 'NONE', #14449 ) ;
#13334=EDGE_CURVE ( 'NONE', #3057, #21013, #15421, .T. ) ;
#13339=CARTESIAN_POINT ( 'NONE',  ( 33.19999999999999574, -85.00000000000000000, 1.200000000000004396 ) ) ;
#13342=ORIENTED_EDGE ( 'NONE', *, *, #4528, .T. ) ;
#13346=DIRECTION ( 'NONE',  ( 0.000000000000000000, 0.000000000000000000, -1.000000000000000000 ) ) ;
#13364=LINE ( 'NONE', #13478, #18002 ) ;
#13367=DIRECTION ( 'NONE',  ( -0.000000000000000000, 1.000000000000000000, -0.000000000000000000 ) ) ;
#13380=ORIENTED_EDGE ( 'NONE', *, *, #4561, .T. ) ;
#13418=CIRCLE ( 'NONE', #18419, 0.3000000000000016542 ) ;
#13421=CARTESIAN_POINT ( 'NONE',  ( -34.39999999999999858, 84.70000000000001705, 0.6000000000000033085 ) ) ;
#13430=EDGE_LOOP ( 'NONE', ( #4430, #16357, #1970, #9334 ) ) ;
#13441=CARTESIAN_POINT ( 'NONE',  ( 30.79999999999999716, -84.70000000000001705, 10.00000000000000178 ) ) ;
#13455=ORIENTED_EDGE ( 'NONE', *, *, #16432, .F. ) ;
#13464=CARTESIAN_POINT ( 'NONE',  ( -33.20000000000000284, 84.70000000000001705, 1.200000000000000400 ) ) ;
#13478=CARTESIAN_POINT ( 'NONE',  ( -33.50000000000000000, 84.70000000000001705, 1.500000000000000000 ) ) ;
#13479=( NAMED_UNIT ( * ) PLANE_ANGLE_UNIT ( ) SI_UNIT ( $, .RADIAN. ) );
#13494=CARTESIAN_POINT ( 'NONE',  ( 34.69999999999999574, -84.70000000000001705, 0.6000000000000033085 ) ) ;
#13502=EDGE_LOOP ( 'NONE', ( #12704, #6991, #16846, #12360 ) ) ;
#13503=CARTESIAN_POINT ( 'NONE',  ( -35.00000000000001421, 85.00000000000000000, 79.39999999999999147 ) ) ;
#13513=DIRECTION ( 'NONE',  ( 0.000000000000000000, 1.000000000000000000, 0.000000000000000000 ) ) ;
#13517=AXIS2_PLACEMENT_3D ( 'NONE', #18430, #9831, #3114 ) ;
#13538=DIRECTION ( 'NONE',  ( 0.000000000000000000, -1.000000000000000000, 0.000000000000000000 ) ) ;
#13552=ORIENTED_EDGE ( 'NONE', *, *, #1205, .F. ) ;
#13559=EDGE_LOOP ( 'NONE', ( #17152, #2465, #12163, #21305 ) ) ;
#13565=CARTESIAN_POINT ( 'NONE',  ( -30.49999999999999289, -85.00000000000000000, 0.3000000000000002665 ) ) ;
#13602=CIRCLE ( 'NONE', #11799, 0.2999999999999947153 ) ;
#13605=DIRECTION ( 'NONE',  ( 0.000000000000000000, 0.000000000000000000, -1.000000000000000000 ) ) ;
#13628=MECHANICAL_DESIGN_GEOMETRIC_PRESENTATION_REPRESENTATION('',(#19036),#12885);
#13633=ADVANCED_FACE ( 'NONE', ( #14222 ), #15557, .T. ) ;
#13637=ORIENTED_EDGE ( 'NONE', *, *, #16057, .F. ) ;
#13650=ADVANCED_FACE ( 'NONE', ( #13999 ), #14097, .T. ) ;
#13655=AXIS2_PLACEMENT_3D ( 'NONE', #14965, #6491, #13284 ) ;
#13664=EDGE_CURVE ( 'NONE', #21087, #17432, #2028, .T. ) ;
#13675=EDGE_LOOP ( 'NONE', ( #18777, #3583, #11914, #16485 ) ) ;
#13680=VERTEX_POINT ( 'NONE', #7095 ) ;
#13681=EDGE_CURVE ( 'NONE', #15917, #19413, #9742, .T. ) ;
#13709=ORIENTED_EDGE ( 'NONE', *, *, #19801, .T. ) ;
#13770=CIRCLE ( 'NONE', #10929, 0.2999999999999999334 ) ;
#13778=CARTESIAN_POINT ( 'NONE',  ( -33.50000000000001421, 84.70000000000001705, 78.20000000000000284 ) ) ;
#13780=ORIENTED_EDGE ( 'NONE', *, *, #11893, .T. ) ;
#13783=CARTESIAN_POINT ( 'NONE',  ( -33.20000000000001705, 85.00000000000000000, 78.50000000000000000 ) ) ;
#13791=ORIENTED_EDGE ( 'NONE', *, *, #16895, .F. ) ;
#13808=DIRECTION ( 'NONE',  ( -6.123233995736766036E-17, 0.000000000000000000, 1.000000000000000000 ) ) ;
#13816=ORIENTED_EDGE ( 'NONE', *, *, #21805, .F. ) ;
#13829=CIRCLE ( 'NONE', #12059, 0.6000000000000033085 ) ;
#13839=ADVANCED_FACE ( 'NONE', ( #14660 ), #12971, .T. ) ;
#13852=DIRECTION ( 'NONE',  ( 1.000000000000000000, -0.000000000000000000, 6.123233995736764803E-17 ) ) ;
#13889=DIRECTION ( 'NONE',  ( 6.123233995736764803E-17, 0.000000000000000000, -1.000000000000000000 ) ) ;
#13915=( NAMED_UNIT ( * ) SI_UNIT ( $, .STERADIAN. ) SOLID_ANGLE_UNIT ( ) );
#13921=VERTEX_POINT ( 'NONE', #22062 ) ;
#13924=DIRECTION ( 'NONE',  ( 1.000000000000000000, 0.000000000000000000, 6.123233995736764803E-17 ) ) ;
#13932=FACE_BOUND ( 'NONE', #9635, .T. ) ;
#13934=CARTESIAN_POINT ( 'NONE',  ( 30.79999999999999716, -85.00000000000000000, 1.734723475976807094E-15 ) ) ;
#13944=CARTESIAN_POINT ( 'NONE',  ( -30.79999999999999361, -123.9599366953518711, 0.2999999999999999334 ) ) ;
#13950=FACE_OUTER_BOUND ( 'NONE', #21137, .T. ) ;
#13955=AXIS2_PLACEMENT_3D ( 'NONE', #6256, #14499, #11587 ) ;
#13958=ORIENTED_EDGE ( 'NONE', *, *, #3701, .T. ) ;
#13969=CARTESIAN_POINT ( 'NONE',  ( -33.20000000000000284, 85.00000000000000000, 1.200000000000000178 ) ) ;
#13977=CARTESIAN_POINT ( 'NONE',  ( 30.79999999999999716, -84.70000000000001705, 1.200000000000004174 ) ) ;
#13992=EDGE_CURVE ( 'NONE', #583, #3057, #3809, .T. ) ;
#13999=FACE_OUTER_BOUND ( 'NONE', #53, .T. ) ;
#14000=CARTESIAN_POINT ( 'NONE',  ( -34.39999999999999858, 84.70000000000001705, 0.3000000000000000444 ) ) ;
#14002=CARTESIAN_POINT ( 'NONE',  ( 34.39999999999998437, -84.70000000000001705, 0.3000000000000042077 ) ) ;
#14031=ORIENTED_EDGE ( 'NONE', *, *, #21723, .T. ) ;
#14032=ORIENTED_EDGE ( 'NONE', *, *, #20859, .F. ) ;
#14033=ORIENTED_EDGE ( 'NONE', *, *, #10842, .F. ) ;
#14042=DIRECTION ( 'NONE',  ( 0.000000000000000000, -1.000000000000000000, 0.000000000000000000 ) ) ;
#14048=ORIENTED_EDGE ( 'NONE', *, *, #15691, .F. ) ;
#14093=CIRCLE ( 'NONE', #5197, 0.3000000000000016542 ) ;
#14097=CYLINDRICAL_SURFACE ( 'NONE', #17585, 0.2999999999999999889 ) ;
#14100=DIRECTION ( 'NONE',  ( -1.000000000000000000, -0.000000000000000000, -0.000000000000000000 ) ) ;
#14102=ORIENTED_EDGE ( 'NONE', *, *, #16871, .T. ) ;
#14103=CARTESIAN_POINT ( 'NONE',  ( 34.99999999999999289, 85.00000000000000000, 79.39999999999999147 ) ) ;
#14108=EDGE_CURVE ( 'NONE', #6971, #13921, #15091, .T. ) ;
#14142=CIRCLE ( 'NONE', #19888, 0.2999999999999947153 ) ;
#14162=FACE_OUTER_BOUND ( 'NONE', #16521, .T. ) ;
#14177=AXIS2_PLACEMENT_3D ( 'NONE', #1427, #20230, #11719 ) ;
#14203=ADVANCED_FACE ( 'NONE', ( #5930 ), #14515, .F. ) ;
#14212=ORIENTED_EDGE ( 'NONE', *, *, #14899, .T. ) ;
#14213=DIRECTION ( 'NONE',  ( -1.000000000000000000, 0.000000000000000000, -6.123233995736764803E-17 ) ) ;
#14219=AXIS2_PLACEMENT_3D ( 'NONE', #6929, #20561, #5239 ) ;
#14222=FACE_OUTER_BOUND ( 'NONE', #15987, .T. ) ;
#14223=EDGE_CURVE ( 'NONE', #5602, #9461, #16880, .T. ) ;
#14236=ORIENTED_EDGE ( 'NONE', *, *, #7174, .T. ) ;
#14238=DIRECTION ( 'NONE',  ( -1.000000000000000000, 0.000000000000000000, 0.000000000000000000 ) ) ;
#14239=AXIS2_PLACEMENT_3D ( 'NONE', #7036, #18773, #20571 ) ;
#14247=VECTOR ( 'NONE', #5898, 1000.000000000000000 ) ;
#14264=EDGE_LOOP ( 'NONE', ( #10141, #6353, #11944 ) ) ;
#14303=ORIENTED_EDGE ( 'NONE', *, *, #1782, .F. ) ;
#14311=CIRCLE ( 'NONE', #20404, 0.2999999999999999334 ) ;
#14324=DIRECTION ( 'NONE',  ( 1.000000000000000000, -0.000000000000000000, -0.000000000000000000 ) ) ;
#14337=ORIENTED_EDGE ( 'NONE', *, *, #16756, .F. ) ;
#14340=( NAMED_UNIT ( * ) SI_UNIT ( $, .STERADIAN. ) SOLID_ANGLE_UNIT ( ) );
#14350=ORIENTED_EDGE ( 'NONE', *, *, #876, .F. ) ;
#14365=ORIENTED_EDGE ( 'NONE', *, *, #6092, .F. ) ;
#14369=ORIENTED_EDGE ( 'NONE', *, *, #15152, .F. ) ;
#14374=DIRECTION ( 'NONE',  ( -0.000000000000000000, 1.000000000000000000, -0.000000000000000000 ) ) ;
#14378=LINE ( 'NONE', #21229, #14247 ) ;
#14386=CARTESIAN_POINT ( 'NONE',  ( 34.39999999999998437, -85.00000000000000000, 0.3000000000000042077 ) ) ;
#14395=ORIENTED_EDGE ( 'NONE', *, *, #6480, .T. ) ;
#14406=ADVANCED_FACE ( 'NONE', ( #11908 ), #6914, .T. ) ;
#14433=CARTESIAN_POINT ( 'NONE',  ( -35.00000000000000000, -84.70000000000001705, 0.2999999999999999889 ) ) ;
#14449=CARTESIAN_POINT ( 'NONE',  ( -34.70000000000001705, -85.00000000000000000, 79.39999999999999147 ) ) ;
#14450=CARTESIAN_POINT ( 'NONE',  ( 30.79999999999999716, -84.70000000000001705, 0.3000000000000039857 ) ) ;
#14457=ORIENTED_EDGE ( 'NONE', *, *, #15691, .T. ) ;
#14462=DIRECTION ( 'NONE',  ( -1.000000000000000000, 0.000000000000000000, 0.000000000000000000 ) ) ;
#14468=CARTESIAN_POINT ( 'NONE',  ( 0.000000000000000000, -84.70000000000001705, 78.79999999999999716 ) ) ;
#14481=ORIENTED_EDGE ( 'NONE', *, *, #7174, .F. ) ;
#14491=VERTEX_POINT ( 'NONE', #10893 ) ;
#14499=DIRECTION ( 'NONE',  ( 0.000000000000000000, -1.000000000000000000, 0.000000000000000000 ) ) ;
#14504=AXIS2_PLACEMENT_3D ( 'NONE', #9809, #22134, #13605 ) ;
#14515=CYLINDRICAL_SURFACE ( 'NONE', #13302, 0.2999999999999947153 ) ;
#14536=AXIS2_PLACEMENT_3D ( 'NONE', #13441, #20282, #8867 ) ;
#14538=AXIS2_PLACEMENT_3D ( 'NONE', #11280, #21496, #9839 ) ;
#14550=ORIENTED_EDGE ( 'NONE', *, *, #16950, .F. ) ;
#14563=AXIS2_PLACEMENT_3D ( 'NONE', #20488, #14996, #4810 ) ;
#14595=EDGE_CURVE ( 'NONE', #8145, #7855, #16029, .T. ) ;
#14613=CARTESIAN_POINT ( 'NONE',  ( -34.40000000000001279, -85.00000000000000000, 79.70000000000000284 ) ) ;
#14616=CARTESIAN_POINT ( 'NONE',  ( -1.836970198721042383E-17, 84.70000000000001705, 0.3000000000000021538 ) ) ;
#14639=DIRECTION ( 'NONE',  ( -8.673617379884034239E-17, -0.000000000000000000, 1.000000000000000000 ) ) ;
#14649=FACE_OUTER_BOUND ( 'NONE', #872, .T. ) ;
#14651=DIRECTION ( 'NONE',  ( 1.000000000000000000, 0.000000000000000000, 0.000000000000000000 ) ) ;
#14660=FACE_OUTER_BOUND ( 'NONE', #368, .T. ) ;
#14693=ORIENTED_EDGE ( 'NONE', *, *, #7886, .T. ) ;
#14698=ORIENTED_EDGE ( 'NONE', *, *, #15888, .T. ) ;
#14715=FACE_OUTER_BOUND ( 'NONE', #3794, .T. ) ;
#14719=CARTESIAN_POINT ( 'NONE',  ( 33.49999999999999289, -84.70000000000001705, 1.799999999999996048 ) ) ;
#14724=CIRCLE ( 'NONE', #13655, 0.6000000000000033085 ) ;
#14749=DIRECTION ( 'NONE',  ( -1.000000000000000000, 0.000000000000000000, 0.000000000000000000 ) ) ;
#14763=CARTESIAN_POINT ( 'NONE',  ( 0.000000000000000000, 84.70000000000001705, 79.70000000000000284 ) ) ;
#14764=CARTESIAN_POINT ( 'NONE',  ( 30.19999999999999574, 69.70000000000000284, 1.500000000000003997 ) ) ;
#14799=EDGE_LOOP ( 'NONE', ( #14983, #12960, #5610, #1487 ) ) ;
#14806=CIRCLE ( 'NONE', #1222, 0.3000000000000000444 ) ;
#14820=AXIS2_PLACEMENT_3D ( 'NONE', #13150, #4329, #16268 ) ;
#14826=LINE ( 'NONE', #16168, #5263 ) ;
#14834=ORIENTED_EDGE ( 'NONE', *, *, #3347, .T. ) ;
#14851=CARTESIAN_POINT ( 'NONE',  ( -30.79999999999999361, -84.70000000000001705, 9.999999999999998224 ) ) ;
#14854=AXIS2_PLACEMENT_3D ( 'NONE', #8678, #20648, #15045 ) ;
#14859=VERTEX_POINT ( 'NONE', #15130 ) ;
#14888=AXIS2_PLACEMENT_3D ( 'NONE', #4779, #19778, #8251 ) ;
#14895=AXIS2_PLACEMENT_3D ( 'NONE', #5430, #3969, #14238 ) ;
#14899=EDGE_CURVE ( 'NONE', #17668, #11071, #3285, .T. ) ;
#14906=DIRECTION ( 'NONE',  ( 0.000000000000000000, 0.000000000000000000, -1.000000000000000000 ) ) ;
#14924=CARTESIAN_POINT ( 'NONE',  ( -33.20000000000000284, -84.70000000000001705, 1.800000000000000266 ) ) ;
#14928=CARTESIAN_POINT ( 'NONE',  ( -35.00000000000001421, -84.70000000000001705, 79.39999999999999147 ) ) ;
#14938=ORIENTED_EDGE ( 'NONE', *, *, #19465, .F. ) ;
#14941=CARTESIAN_POINT ( 'NONE',  ( -33.20000000000001705, -84.70000000000001705, 78.20000000000000284 ) ) ;
#14946=VERTEX_POINT ( 'NONE', #2149 ) ;
#14947=ORIENTED_EDGE ( 'NONE', *, *, #17726, .F. ) ;
#14963=PLANE ( 'NONE',  #7397 ) ;
#14964=DIRECTION ( 'NONE',  ( -1.000000000000000000, 0.000000000000000000, 0.000000000000000000 ) ) ;
#14965=CARTESIAN_POINT ( 'NONE',  ( -34.40000000000001279, -84.70000000000001705, 79.39999999999999147 ) ) ;
#14968=DIRECTION ( 'NONE',  ( 0.000000000000000000, -1.084202172485523564E-15, -1.000000000000000000 ) ) ;
#14971=TOROIDAL_SURFACE ( 'NONE', #22141, 0.5999999999999999778, 0.2999999999999999889 ) ;
#14983=ORIENTED_EDGE ( 'NONE', *, *, #12768, .T. ) ;
#14988=CIRCLE ( 'NONE', #7869, 0.3000000000000016542 ) ;
#14990=FACE_OUTER_BOUND ( 'NONE', #1877, .T. ) ;
#14993=ADVANCED_FACE ( 'NONE', ( #10080 ), #6158, .T. ) ;
#14996=DIRECTION ( 'NONE',  ( 0.000000000000000000, -1.000000000000000000, 0.000000000000000000 ) ) ;
#15002=CARTESIAN_POINT ( 'NONE',  ( 33.19999999999999574, -84.70000000000001705, 1.200000000000004174 ) ) ;
#15004=EDGE_CURVE ( 'NONE', #10209, #6583, #108, .T. ) ;
#15010=CYLINDRICAL_SURFACE ( 'NONE', #19581, 0.2999999999999999889 ) ;
#15014=EDGE_CURVE ( 'NONE', #18912, #11071, #6954, .T. ) ;
#15018=VERTEX_POINT ( 'NONE', #12066 ) ;
#15026=DIRECTION ( 'NONE',  ( -0.000000000000000000, 1.000000000000000000, -0.000000000000000000 ) ) ;
#15035=CARTESIAN_POINT ( 'NONE',  ( -33.80000000000001847, -85.00000000000000000, 78.20000000000000284 ) ) ;
#15045=DIRECTION ( 'NONE',  ( 0.000000000000000000, 0.000000000000000000, -1.000000000000000000 ) ) ;
#15052=VERTEX_POINT ( 'NONE', #12170 ) ;
#15074=AXIS2_PLACEMENT_3D ( 'NONE', #4419, #14374, #6228 ) ;
#15086=CARTESIAN_POINT ( 'NONE',  ( 30.19999999999999574, 69.70000000000000284, 0.3000000000000033751 ) ) ;
#15091=CIRCLE ( 'NONE', #9378, 0.3000000000000016542 ) ;
#15092=AXIS2_PLACEMENT_3D ( 'NONE', #4327, #8925, #7360 ) ;
#15121=FACE_OUTER_BOUND ( 'NONE', #15218, .T. ) ;
#15125=CARTESIAN_POINT ( 'NONE',  ( -30.49999999999998934, 69.70000000000001705, 0.2999999999999999334 ) ) ;
#15130=CARTESIAN_POINT ( 'NONE',  ( -33.80000000000000426, 85.00000000000000000, 1.800000000000000266 ) ) ;
#15135=DIRECTION ( 'NONE',  ( -6.123233995736764803E-17, 0.000000000000000000, 1.000000000000000000 ) ) ;
#15138=ORIENTED_EDGE ( 'NONE', *, *, #11252, .F. ) ;
#15143=TOROIDAL_SURFACE ( 'NONE', #21959, 0.5999999999999999778, 0.2999999999999999889 ) ;
#15145=CYLINDRICAL_SURFACE ( 'NONE', #4597, 0.3000000000000016542 ) ;
#15152=EDGE_CURVE ( 'NONE', #18983, #13328, #17232, .T. ) ;
#15169=EDGE_LOOP ( 'NONE', ( #10101, #3378, #10381, #2037 ) ) ;
#15174=CARTESIAN_POINT ( 'NONE',  ( -30.19999999999999574, 69.70000000000001705, 0.2999999999999999334 ) ) ;
#15176=VECTOR ( 'NONE', #13889, 1000.000000000000000 ) ;
#15192=CARTESIAN_POINT ( 'NONE',  ( -35.00000000000000000, 85.00000000000000000, 1.500000000000000000 ) ) ;
#15214=AXIS2_PLACEMENT_3D ( 'NONE', #11122, #18048, #18285 ) ;
#15216=ORIENTED_EDGE ( 'NONE', *, *, #18615, .F. ) ;
#15217=VECTOR ( 'NONE', #20619, 1000.000000000000000 ) ;
#15218=EDGE_LOOP ( 'NONE', ( #18657, #15876, #8004, #20830 ) ) ;
#15230=DIRECTION ( 'NONE',  ( 0.000000000000000000, 0.000000000000000000, -1.000000000000000000 ) ) ;
#15237=LINE ( 'NONE', #13565, #5764 ) ;
#15247=FACE_OUTER_BOUND ( 'NONE', #18111, .T. ) ;
#15249=EDGE_CURVE ( 'NONE', #9143, #20684, #793, .T. ) ;
#15250=AXIS2_PLACEMENT_3D ( 'NONE', #15378, #10785, #3736 ) ;
#15254=AXIS2_PLACEMENT_3D ( 'NONE', #11597, #14968, #20355 ) ;
#15255=AXIS2_PLACEMENT_3D ( 'NONE', #9786, #4644, #13346 ) ;
#15271=CARTESIAN_POINT ( 'NONE',  ( -35.00000000000000000, 84.70000000000001705, 1.200000000000000178 ) ) ;
#15272=ORIENTED_EDGE ( 'NONE', *, *, #20574, .F. ) ;
#15276=ORIENTED_EDGE ( 'NONE', *, *, #20507, .F. ) ;
#15281=CARTESIAN_POINT ( 'NONE',  ( 33.19999999999999574, 85.00000000000000000, 78.20000000000000284 ) ) ;
#15288=ORIENTED_EDGE ( 'NONE', *, *, #876, .T. ) ;
#15299=AXIS2_PLACEMENT_3D ( 'NONE', #5969, #12979, #800 ) ;
#15312=AXIS2_PLACEMENT_3D ( 'NONE', #15576, #16016, #10882 ) ;
#15313=CIRCLE ( 'NONE', #7112, 0.6000000000000033085 ) ;
#15326=LINE ( 'NONE', #10178, #18126 ) ;
#15339=CARTESIAN_POINT ( 'NONE',  ( 34.39999999999998437, -84.70000000000001705, 80.00000000000000000 ) ) ;
#15362=VERTEX_POINT ( 'NONE', #16628 ) ;
#15366=EDGE_CURVE ( 'NONE', #18983, #17660, #14724, .T. ) ;
#15373=CIRCLE ( 'NONE', #5752, 0.3000000000000016542 ) ;
#15378=CARTESIAN_POINT ( 'NONE',  ( 30.19999999999999574, 70.29999999999999716, 0.3000000000000033751 ) ) ;
#15380=ORIENTED_EDGE ( 'NONE', *, *, #19179, .F. ) ;
#15387=FACE_OUTER_BOUND ( 'NONE', #13430, .T. ) ;
#15410=DIRECTION ( 'NONE',  ( 0.000000000000000000, -1.000000000000000000, 0.000000000000000000 ) ) ;
#15419=DIRECTION ( 'NONE',  ( -6.123233995736764803E-17, -0.000000000000000000, 1.000000000000000000 ) ) ;
#15421=CIRCLE ( 'NONE', #7569, 0.2999999999999947153 ) ;
#15462=DIRECTION ( 'NONE',  ( -0.000000000000000000, 1.000000000000000000, -0.000000000000000000 ) ) ;
#15466=ADVANCED_FACE ( 'NONE', ( #15505 ), #3333, .T. ) ;
#15484=DIRECTION ( 'NONE',  ( 0.000000000000000000, -1.000000000000000000, 0.000000000000000000 ) ) ;
#15486=SURFACE_STYLE_USAGE ( .BOTH. , #10132 ) ;
#15487=PLANE ( 'NONE',  #552 ) ;
#15496=DIRECTION ( 'NONE',  ( 0.000000000000000000, 0.000000000000000000, -1.000000000000000000 ) ) ;
#15505=FACE_OUTER_BOUND ( 'NONE', #15942, .T. ) ;
#15508=SPHERICAL_SURFACE ( 'NONE', #6407, 0.2999999999999999889 ) ;
#15510=EDGE_CURVE ( 'NONE', #10209, #15362, #2337, .T. ) ;
#15512=DIRECTION ( 'NONE',  ( 0.000000000000000000, 0.000000000000000000, -1.000000000000000000 ) ) ;
#15516=DIRECTION ( 'NONE',  ( 0.000000000000000000, 0.000000000000000000, 1.000000000000000000 ) ) ;
#15517=ORIENTED_EDGE ( 'NONE', *, *, #6830, .F. ) ;
#15520=ORIENTED_EDGE ( 'NONE', *, *, #1205, .T. ) ;
#15551=CARTESIAN_POINT ( 'NONE',  ( 34.99999999999999289, -84.70000000000001705, 0.6000000000000033085 ) ) ;
#15557=CYLINDRICAL_SURFACE ( 'NONE', #2217, 0.3000000000000016542 ) ;
#15558=DIRECTION ( 'NONE',  ( -1.000000000000000000, 0.000000000000000000, 0.000000000000000000 ) ) ;
#15560=AXIS2_PLACEMENT_3D ( 'NONE', #5030, #1432, #8168 ) ;
#15565=AXIS2_PLACEMENT_3D ( 'NONE', #20861, #5657, #7323 ) ;
#15572=CIRCLE ( 'NONE', #4501, 0.2999999999999947153 ) ;
#15576=CARTESIAN_POINT ( 'NONE',  ( 33.19999999999999574, 85.00000000000000000, 1.799999999999996048 ) ) ;
#15608=CIRCLE ( 'NONE', #21357, 0.6000000000000033085 ) ;
#15610=CIRCLE ( 'NONE', #19555, 0.3000000000000016542 ) ;
#15630=CIRCLE ( 'NONE', #11710, 0.2999999999999999889 ) ;
#15635=TOROIDAL_SURFACE ( 'NONE', #9584, 0.2999999999999999889, 0.2999999999999999889 ) ;
#15645=UNCERTAINTY_MEASURE_WITH_UNIT (LENGTH_MEASURE( 1.000000000000000082E-05 ), #12874, 'distance_accuracy_value', 'NONE');
#15663=VERTEX_POINT ( 'NONE', #21454 ) ;
#15664=EDGE_CURVE ( 'NONE', #4617, #21291, #19650, .T. ) ;
#15675=DIRECTION ( 'NONE',  ( -1.734723475976806848E-16, 0.000000000000000000, 1.000000000000000000 ) ) ;
#15689=EDGE_LOOP ( 'NONE', ( #12133, #20618, #16539, #9023 ) ) ;
#15691=EDGE_CURVE ( 'NONE', #5083, #10170, #20222, .T. ) ;
#15726=EDGE_CURVE ( 'NONE', #17432, #13921, #3434, .T. ) ;
#15731=AXIS2_PLACEMENT_3D ( 'NONE', #5326, #12735, #19589 ) ;
#15739=FACE_OUTER_BOUND ( 'NONE', #7550, .T. ) ;
#15757=EDGE_CURVE ( 'NONE', #13328, #1975, #6014, .T. ) ;
#15777=LINE ( 'NONE', #15551, #15217 ) ;
#15778=CARTESIAN_POINT ( 'NONE',  ( -34.40000000000001279, 84.70000000000001705, 79.39999999999999147 ) ) ;
#15786=DIRECTION ( 'NONE',  ( 0.000000000000000000, 0.000000000000000000, -1.000000000000000000 ) ) ;
#15793=DIRECTION ( 'NONE',  ( 0.000000000000000000, -1.000000000000000000, 0.000000000000000000 ) ) ;
#15796=ORIENTED_EDGE ( 'NONE', *, *, #1937, .T. ) ;
#15812=ORIENTED_EDGE ( 'NONE', *, *, #18196, .T. ) ;
#15834=CARTESIAN_POINT ( 'NONE',  ( -30.49999999999999289, -85.00000000000000000, 1.199999999999999734 ) ) ;
#15851=ORIENTED_EDGE ( 'NONE', *, *, #9967, .T. ) ;
#15865=EDGE_CURVE ( 'NONE', #10431, #17181, #18735, .T. ) ;
#15867=VECTOR ( 'NONE', #13086, 1000.000000000000000 ) ;
#15869=DIRECTION ( 'NONE',  ( 0.000000000000000000, -1.000000000000000000, 0.000000000000000000 ) ) ;
#15876=ORIENTED_EDGE ( 'NONE', *, *, #15865, .F. ) ;
#15879=DIRECTION ( 'NONE',  ( 1.000000000000000000, 0.000000000000000000, 0.000000000000000000 ) ) ;
#15888=EDGE_CURVE ( 'NONE', #17660, #10999, #17015, .T. ) ;
#15912=AXIS2_PLACEMENT_3D ( 'NONE', #177, #10488, #8603 ) ;
#15917=VERTEX_POINT ( 'NONE', #10787 ) ;
#15925=EDGE_CURVE ( 'NONE', #6698, #7599, #12700, .T. ) ;
#15926=EDGE_CURVE ( 'NONE', #5394, #12260, #5868, .T. ) ;
#15940=CARTESIAN_POINT ( 'NONE',  ( -35.00000000000001421, 84.70000000000001705, 79.39999999999999147 ) ) ;
#15942=EDGE_LOOP ( 'NONE', ( #20485, #11115, #15380, #12478 ) ) ;
#15949=DIRECTION ( 'NONE',  ( 0.000000000000000000, 0.000000000000000000, -1.000000000000000000 ) ) ;
#15951=VERTEX_POINT ( 'NONE', #697 ) ;
#15977=DIRECTION ( 'NONE',  ( 0.000000000000000000, -1.000000000000000000, 0.000000000000000000 ) ) ;
#15984=CARTESIAN_POINT ( 'NONE',  ( 33.49999999999999289, -85.00000000000000000, 1.799999999999996048 ) ) ;
#15987=EDGE_LOOP ( 'NONE', ( #10286, #9740, #18741, #16307 ) ) ;
#16011=ORIENTED_EDGE ( 'NONE', *, *, #2550, .F. ) ;
#16016=DIRECTION ( 'NONE',  ( 0.000000000000000000, 1.000000000000000000, 0.000000000000000000 ) ) ;
#16029=LINE ( 'NONE', #17825, #10063 ) ;
#16039=CARTESIAN_POINT ( 'NONE',  ( -33.20000000000001705, 85.00000000000000000, 78.20000000000000284 ) ) ;
#16057=EDGE_CURVE ( 'NONE', #3754, #15018, #12988, .T. ) ;
#16059=CIRCLE ( 'NONE', #10721, 0.2999999999999999889 ) ;
#16089=VECTOR ( 'NONE', #17967, 1000.000000000000000 ) ;
#16092=AXIS2_PLACEMENT_3D ( 'NONE', #21971, #8320, #6877 ) ;
#16101=CARTESIAN_POINT ( 'NONE',  ( 34.69999999999998863, -84.70000000000001705, 80.00000000000000000 ) ) ;
#16107=EDGE_CURVE ( 'NONE', #13680, #10431, #7763, .T. ) ;
#16111=FACE_OUTER_BOUND ( 'NONE', #8107, .T. ) ;
#16121=PRODUCT_DEFINITION ( 'UNKNOWN', '', #3721, #3803 ) ;
#16122=ORIENTED_EDGE ( 'NONE', *, *, #11046, .F. ) ;
#16132=FACE_OUTER_BOUND ( 'NONE', #3424, .T. ) ;
#16135=CARTESIAN_POINT ( 'NONE',  ( 33.19999999999999574, -85.00000000000000000, 78.79999999999999716 ) ) ;
#16150=DIRECTION ( 'NONE',  ( -0.000000000000000000, 1.000000000000000000, -0.000000000000000000 ) ) ;
#16160=DIRECTION ( 'NONE',  ( 0.000000000000000000, -1.000000000000000000, 0.000000000000000000 ) ) ;
#16168=CARTESIAN_POINT ( 'NONE',  ( -33.80000000000000426, -85.00000000000000000, -5.863365348801607979E-15 ) ) ;
#16200=ORIENTED_EDGE ( 'NONE', *, *, #19476, .F. ) ;
#16222=SURFACE_STYLE_USAGE ( .BOTH. , #9423 ) ;
#16226=DIRECTION ( 'NONE',  ( 1.000000000000000000, 0.000000000000000000, 0.000000000000000000 ) ) ;
#16232=ORIENTED_EDGE ( 'NONE', *, *, #9663, .F. ) ;
#16268=DIRECTION ( 'NONE',  ( 1.000000000000000000, 0.000000000000000000, 6.123233995736766036E-17 ) ) ;
#16273=ORIENTED_EDGE ( 'NONE', *, *, #15925, .F. ) ;
#16291=DIRECTION ( 'NONE',  ( 1.000000000000000000, 0.000000000000000000, 0.000000000000000000 ) ) ;
#16301=DIRECTION ( 'NONE',  ( 0.000000000000000000, 0.000000000000000000, -1.000000000000000000 ) ) ;
#16307=ORIENTED_EDGE ( 'NONE', *, *, #8421, .F. ) ;
#16308=VECTOR ( 'NONE', #579, 1000.000000000000000 ) ;
#16347=CARTESIAN_POINT ( 'NONE',  ( -33.20000000000001705, -85.00000000000000000, 78.79999999999999716 ) ) ;
#16357=ORIENTED_EDGE ( 'NONE', *, *, #1972, .F. ) ;
#16367=DIRECTION ( 'NONE',  ( 0.000000000000000000, -1.000000000000000000, 0.000000000000000000 ) ) ;
#16379=CARTESIAN_POINT ( 'NONE',  ( -33.80000000000000426, -84.70000000000001705, 1.800000000000000266 ) ) ;
#16410=DIRECTION ( 'NONE',  ( -1.000000000000000000, 0.000000000000000000, -6.123233995736764803E-17 ) ) ;
#16417=LINE ( 'NONE', #8037, #10765 ) ;
#16431=ORIENTED_EDGE ( 'NONE', *, *, #15014, .T. ) ;
#16432=EDGE_CURVE ( 'NONE', #1780, #3156, #1665, .T. ) ;
#16440=ORIENTED_EDGE ( 'NONE', *, *, #12958, .T. ) ;
#16451=AXIS2_PLACEMENT_3D ( 'NONE', #16822, #17163, #12000 ) ;
#16485=ORIENTED_EDGE ( 'NONE', *, *, #11973, .F. ) ;
#16502=CARTESIAN_POINT ( 'NONE',  ( -33.20000000000001705, 84.70000000000001705, 78.20000000000000284 ) ) ;
#16507=FACE_OUTER_BOUND ( 'NONE', #20000, .T. ) ;
#16521=EDGE_LOOP ( 'NONE', ( #21356, #21750, #3345, #7207, #19322, #14365, #7032, #12161, #3193, #10257 ) ) ;
#16539=ORIENTED_EDGE ( 'NONE', *, *, #5563, .F. ) ;
#16544=CARTESIAN_POINT ( 'NONE',  ( -34.40000000000001279, 84.70000000000001705, 79.39999999999999147 ) ) ;
#16562=CARTESIAN_POINT ( 'NONE',  ( -30.79999999999999361, -84.70000000000001705, 1.500000000000000222 ) ) ;
#16578=CARTESIAN_POINT ( 'NONE',  ( 33.49999999999998579, -84.70000000000001705, 78.20000000000000284 ) ) ;
#16599=EDGE_CURVE ( 'NONE', #6840, #10124, #22071, .T. ) ;
#16628=CARTESIAN_POINT ( 'NONE',  ( -33.20000000000001705, -84.70000000000001705, 78.50000000000000000 ) ) ;
#16647=ADVANCED_FACE ( 'NONE', ( #9599 ), #7819, .T. ) ;
#16653=ORIENTED_EDGE ( 'NONE', *, *, #7886, .F. ) ;
#16669=VECTOR ( 'NONE', #9945, 1000.000000000000000 ) ;
#16673=CYLINDRICAL_SURFACE ( 'NONE', #18874, 0.3000000000000016542 ) ;
#16681=EDGE_LOOP ( 'NONE', ( #18736, #8833, #1085, #1901 ) ) ;
#16703=VERTEX_POINT ( 'NONE', #13271 ) ;
#16726=FACE_OUTER_BOUND ( 'NONE', #6506, .T. ) ;
#16747=AXIS2_PLACEMENT_3D ( 'NONE', #21158, #8688, #22004 ) ;
#16756=EDGE_CURVE ( 'NONE', #21431, #3754, #8121, .T. ) ;
#16762=AXIS2_PLACEMENT_3D ( 'NONE', #1607, #9799, #18514 ) ;
#16767=ORIENTED_EDGE ( 'NONE', *, *, #15152, .T. ) ;
#16774=DIRECTION ( 'NONE',  ( 1.000000000000000000, 0.000000000000000000, 6.123233995736701941E-17 ) ) ;
#16779=ADVANCED_FACE ( 'NONE', ( #17284 ), #22011, .T. ) ;
#16795=CARTESIAN_POINT ( 'NONE',  ( -34.40000000000001279, -84.70000000000001705, 80.00000000000000000 ) ) ;
#16822=CARTESIAN_POINT ( 'NONE',  ( -34.39999999999999858, -84.70000000000001705, 0.6000000000000033085 ) ) ;
#16839=ORIENTED_EDGE ( 'NONE', *, *, #7127, .F. ) ;
#16846=ORIENTED_EDGE ( 'NONE', *, *, #17253, .F. ) ;
#16870=CARTESIAN_POINT ( 'NONE',  ( 30.50000000000000000, 70.29999999999999716, 1.500000000000003997 ) ) ;
#16871=EDGE_CURVE ( 'NONE', #5205, #2890, #4082, .T. ) ;
#16872=CYLINDRICAL_SURFACE ( 'NONE', #15560, 0.3000000000000016542 ) ;
#16876=ORIENTED_EDGE ( 'NONE', *, *, #16895, .T. ) ;
#16877=EDGE_LOOP ( 'NONE', ( #1928, #12167, #14481, #7234 ) ) ;
#16880=CIRCLE ( 'NONE', #5819, 0.2999999999999999889 ) ;
#16882=COLOUR_RGB ( '', 0.40784314, 0.44705882, 0.49803922) ;
#16895=EDGE_CURVE ( 'NONE', #17181, #3127, #21215, .T. ) ;
#16919=CARTESIAN_POINT ( 'NONE',  ( -35.00000000000000000, 84.70000000000001705, 0.000000000000000000 ) ) ;
#16943=CARTESIAN_POINT ( 'NONE',  ( 34.39999999999998437, -84.70000000000001705, 79.39999999999999147 ) ) ;
#16950=EDGE_CURVE ( 'NONE', #17432, #5083, #5884, .T. ) ;
#16951=ORIENTED_EDGE ( 'NONE', *, *, #12542, .T. ) ;
#16954=EDGE_LOOP ( 'NONE', ( #843, #18480, #20984, #21115 ) ) ;
#17004=DIRECTION ( 'NONE',  ( 0.000000000000000000, 0.000000000000000000, -1.000000000000000000 ) ) ;
#17012=CARTESIAN_POINT ( 'NONE',  ( -35.00000000000001421, 84.70000000000001705, 80.00000000000000000 ) ) ;
#17015=CIRCLE ( 'NONE', #14854, 0.2999999999999947153 ) ;
#17035=EDGE_CURVE ( 'NONE', #12623, #12088, #10637, .T. ) ;
#17053=CARTESIAN_POINT ( 'NONE',  ( -30.79999999999999361, -123.9599366953518711, 1.199999999999999734 ) ) ;
#17087=ADVANCED_FACE ( 'NONE', ( #18045 ), #7072, .T. ) ;
#17088=ORIENTED_EDGE ( 'NONE', *, *, #1782, .T. ) ;
#17094=VECTOR ( 'NONE', #15793, 1000.000000000000000 ) ;
#17100=CARTESIAN_POINT ( 'NONE',  ( 30.79999999999999716, -84.70000000000001705, 0.3000000000000033751 ) ) ;
#17107=CARTESIAN_POINT ( 'NONE',  ( -34.40000000000001279, 85.00000000000000000, 80.00000000000000000 ) ) ;
#17121=FACE_OUTER_BOUND ( 'NONE', #16681, .T. ) ;
#17125=DIRECTION ( 'NONE',  ( -0.000000000000000000, 1.000000000000000000, 0.000000000000000000 ) ) ;
#17141=FACE_OUTER_BOUND ( 'NONE', #4741, .T. ) ;
#17143=CARTESIAN_POINT ( 'NONE',  ( -34.40000000000001279, 85.00000000000000000, 79.39999999999999147 ) ) ;
#17145=LINE ( 'NONE', #16919, #6198 ) ;
#17152=ORIENTED_EDGE ( 'NONE', *, *, #733, .T. ) ;
#17155=DIRECTION ( 'NONE',  ( -6.123233995736764803E-17, -0.000000000000000000, 1.000000000000000000 ) ) ;
#17157=ADVANCED_FACE ( 'NONE', ( #15247 ), #9208, .T. ) ;
#17163=DIRECTION ( 'NONE',  ( -0.000000000000000000, 1.000000000000000000, -0.000000000000000000 ) ) ;
#17181=VERTEX_POINT ( 'NONE', #20635 ) ;
#17184=CARTESIAN_POINT ( 'NONE',  ( 0.000000000000000000, 85.00000000000000000, 79.70000000000000284 ) ) ;
#17185=DIRECTION ( 'NONE',  ( 0.000000000000000000, -1.000000000000000000, 0.000000000000000000 ) ) ;
#17189=EDGE_CURVE ( 'NONE', #6840, #14859, #6659, .T. ) ;
#17201=CARTESIAN_POINT ( 'NONE',  ( 33.19999999999999574, -84.70000000000001705, 1.799999999999996048 ) ) ;
#17229=ADVANCED_FACE ( 'NONE', ( #8224 ), #3183, .T. ) ;
#17232=CIRCLE ( 'NONE', #8305, 0.3000000000000016542 ) ;
#17240=AXIS2_PLACEMENT_3D ( 'NONE', #2479, #21516, #891 ) ;
#17253=EDGE_CURVE ( 'NONE', #8060, #814, #8765, .T. ) ;
#17263=CARTESIAN_POINT ( 'NONE',  ( 33.50000000000000000, 85.00000000000000000, 1.200000000000004174 ) ) ;
#17264=STYLED_ITEM ( 'NONE', ( #899 ), #13111 ) ;
#17271=PRESENTATION_STYLE_ASSIGNMENT (( #15486 ) ) ;
#17284=FACE_OUTER_BOUND ( 'NONE', #20609, .T. ) ;
#17305=EDGE_LOOP ( 'NONE', ( #6636, #4586, #21434, #18278 ) ) ;
#17307=DIRECTION ( 'NONE',  ( -1.000000000000000000, 0.000000000000000000, -0.000000000000000000 ) ) ;
#17321=DIRECTION ( 'NONE',  ( 0.000000000000000000, -1.000000000000000000, 0.000000000000000000 ) ) ;
#17335=DIRECTION ( 'NONE',  ( -1.000000000000000000, 0.000000000000000000, 0.000000000000000000 ) ) ;
#17350=LINE ( 'NONE', #4355, #11023 ) ;
#17357=AXIS2_PLACEMENT_3D ( 'NONE', #4312, #17837, #4198 ) ;
#17399=ORIENTED_EDGE ( 'NONE', *, *, #5957, .F. ) ;
#17406=DIRECTION ( 'NONE',  ( 1.000000000000000000, 0.000000000000000000, 0.000000000000000000 ) ) ;
#17408=VECTOR ( 'NONE', #14639, 1000.000000000000000 ) ;
#17432=VERTEX_POINT ( 'NONE', #16562 ) ;
#17441=ADVANCED_FACE ( 'NONE', ( #21413 ), #12756, .T. ) ;
#17473=CARTESIAN_POINT ( 'NONE',  ( 33.19999999999999574, -85.00000000000000000, 78.20000000000000284 ) ) ;
#17477=DIRECTION ( 'NONE',  ( -1.000000000000000000, 0.000000000000000000, 0.000000000000000000 ) ) ;
#17493=AXIS2_PLACEMENT_3D ( 'NONE', #9767, #1237, #16226 ) ;
#17494=CIRCLE ( 'NONE', #19292, 0.3000000000000016542 ) ;
#17501=DIRECTION ( 'NONE',  ( 0.000000000000000000, 0.000000000000000000, -1.000000000000000000 ) ) ;
#17515=AXIS2_PLACEMENT_3D ( 'NONE', #18765, #15410, #13176 ) ;
#17516=ORIENTED_EDGE ( 'NONE', *, *, #15926, .T. ) ;
#17530=DIRECTION ( 'NONE',  ( 0.000000000000000000, -1.000000000000000000, 0.000000000000000000 ) ) ;
#17540=CARTESIAN_POINT ( 'NONE',  ( -30.79999999999999361, -85.00000000000000000, 1.499999999999999556 ) ) ;
#17548=CIRCLE ( 'NONE', #13256, 0.2999999999999947153 ) ;
#17556=CIRCLE ( 'NONE', #15092, 0.2999999999999999334 ) ;
#17579=CARTESIAN_POINT ( 'NONE',  ( -33.20000000000001705, 84.70000000000001705, 78.20000000000000284 ) ) ;
#17581=CARTESIAN_POINT ( 'NONE',  ( -30.19999999999999574, 69.70000000000001705, 9.999999999999998224 ) ) ;
#17584=APPLICATION_CONTEXT ( 'automotive_design' ) ;
#17585=AXIS2_PLACEMENT_3D ( 'NONE', #12532, #19479, #20845 ) ;
#17598=ORIENTED_EDGE ( 'NONE', *, *, #17253, .T. ) ;
#17617=EDGE_CURVE ( 'NONE', #15052, #823, #3264, .T. ) ;
#17626=CARTESIAN_POINT ( 'NONE',  ( 34.39999999999998437, 85.00000000000000000, 80.00000000000000000 ) ) ;
#17630=CARTESIAN_POINT ( 'NONE',  ( -34.39999999999999858, -84.70000000000001705, 0.6000000000000033085 ) ) ;
#17649=AXIS2_PLACEMENT_3D ( 'NONE', #3473, #17125, #8297 ) ;
#17652=DIRECTION ( 'NONE',  ( 1.000000000000000000, 0.000000000000000000, 0.000000000000000000 ) ) ;
#17660=VERTEX_POINT ( 'NONE', #16795 ) ;
#17664=ORIENTED_EDGE ( 'NONE', *, *, #19128, .F. ) ;
#17668=VERTEX_POINT ( 'NONE', #7516 ) ;
#17675=LINE ( 'NONE', #9186, #13072 ) ;
#17692=AXIS2_PLACEMENT_3D ( 'NONE', #20765, #5545, #1848 ) ;
#17700=EDGE_LOOP ( 'NONE', ( #13958, #6977, #21819, #13300 ) ) ;
#17710=VECTOR ( 'NONE', #2604, 1000.000000000000000 ) ;
#17720=EDGE_CURVE ( 'NONE', #15951, #16703, #4605, .T. ) ;
#17723=CIRCLE ( 'NONE', #3797, 0.2999999999999947153 ) ;
#17725=AXIS2_PLACEMENT_3D ( 'NONE', #17795, #2475, #11082 ) ;
#17726=EDGE_CURVE ( 'NONE', #6175, #21952, #9065, .T. ) ;
#17770=VERTEX_POINT ( 'NONE', #5736 ) ;
#17773=DIRECTION ( 'NONE',  ( -0.000000000000000000, 1.000000000000000000, -0.000000000000000000 ) ) ;
#17794=DIRECTION ( 'NONE',  ( 0.000000000000000000, 0.000000000000000000, 1.000000000000000000 ) ) ;
#17795=CARTESIAN_POINT ( 'NONE',  ( -33.20000000000000284, 84.70000000000001705, 1.800000000000000266 ) ) ;
#17819=CARTESIAN_POINT ( 'NONE',  ( 30.19999999999999574, 69.70000000000000284, 1.200000000000003064 ) ) ;
#17825=CARTESIAN_POINT ( 'NONE',  ( 33.79999999999999005, 85.00000000000000000, 78.50000000000000000 ) ) ;
#17830=VERTEX_POINT ( 'NONE', #4468 ) ;
#17837=DIRECTION ( 'NONE',  ( 0.000000000000000000, 0.000000000000000000, -1.000000000000000000 ) ) ;
#17881=EDGE_CURVE ( 'NONE', #21087, #4692, #6039, .T. ) ;
#17915=ORIENTED_EDGE ( 'NONE', *, *, #17720, .T. ) ;
#17917=SURFACE_STYLE_FILL_AREA ( #11096 ) ;
#17923=VECTOR ( 'NONE', #8979, 1000.000000000000000 ) ;
#17927=AXIS2_PLACEMENT_3D ( 'NONE', #14763, #21505, #6177 ) ;
#17928=DIRECTION ( 'NONE',  ( 0.000000000000000000, -1.000000000000000000, 0.000000000000000000 ) ) ;
#17935=DIRECTION ( 'NONE',  ( -1.000000000000000000, 0.000000000000000000, 0.000000000000000000 ) ) ;
#17940=ORIENTED_EDGE ( 'NONE', *, *, #8118, .T. ) ;
#17967=DIRECTION ( 'NONE',  ( 0.000000000000000000, -1.000000000000000000, 0.000000000000000000 ) ) ;
#17970=CARTESIAN_POINT ( 'NONE',  ( 33.19999999999999574, -84.70000000000001705, 78.50000000000000000 ) ) ;
#17975=DIRECTION ( 'NONE',  ( 0.000000000000000000, 0.000000000000000000, -1.000000000000000000 ) ) ;
#17987=CARTESIAN_POINT ( 'NONE',  ( -30.49999999999999289, -123.9599366953518711, 0.2999999999999999334 ) ) ;
#18002=VECTOR ( 'NONE', #6908, 1000.000000000000000 ) ;
#18011=ADVANCED_FACE ( 'NONE', ( #8383 ), #8058, .T. ) ;
#18012=FACE_OUTER_BOUND ( 'NONE', #14799, .T. ) ;
#18014=LINE ( 'NONE', #13083, #1567 ) ;
#18026=EDGE_CURVE ( 'NONE', #15663, #8641, #12057, .T. ) ;
#18031=CARTESIAN_POINT ( 'NONE',  ( -34.39999999999999858, -84.70000000000001705, 5.421010862427522170E-17 ) ) ;
#18045=FACE_OUTER_BOUND ( 'NONE', #20886, .T. ) ;
#18047=ORIENTED_EDGE ( 'NONE', *, *, #18176, .T. ) ;
#18048=DIRECTION ( 'NONE',  ( 0.000000000000000000, -1.000000000000000000, 0.000000000000000000 ) ) ;
#18059=DIRECTION ( 'NONE',  ( 1.000000000000000000, 0.000000000000000000, -0.000000000000000000 ) ) ;
#18073=VECTOR ( 'NONE', #3896, 1000.000000000000000 ) ;
#18074=VECTOR ( 'NONE', #20475, 1000.000000000000000 ) ;
#18082=EDGE_CURVE ( 'NONE', #12578, #19724, #19923, .T. ) ;
#18085=FACE_OUTER_BOUND ( 'NONE', #13502, .T. ) ;
#18088=CARTESIAN_POINT ( 'NONE',  ( 34.99999999999999289, 85.00000000000000000, 80.00000000000000000 ) ) ;
#18111=EDGE_LOOP ( 'NONE', ( #9661, #15812, #5497, #11759 ) ) ;
#18113=ADVANCED_FACE ( 'NONE', ( #14990 ), #21507, .F. ) ;
#18126=VECTOR ( 'NONE', #20374, 1000.000000000000000 ) ;
#18145=ORIENTED_EDGE ( 'NONE', *, *, #12349, .T. ) ;
#18163=CARTESIAN_POINT ( 'NONE',  ( 33.19999999999999574, 85.00000000000000000, 1.500000000000004219 ) ) ;
#18176=EDGE_CURVE ( 'NONE', #7001, #6175, #8289, .T. ) ;
#18190=DIRECTION ( 'NONE',  ( 0.000000000000000000, 0.000000000000000000, -1.000000000000000000 ) ) ;
#18195=CARTESIAN_POINT ( 'NONE',  ( -33.20000000000000284, -85.00000000000000000, 1.500000000000000000 ) ) ;
#18196=EDGE_CURVE ( 'NONE', #21163, #14946, #3833, .T. ) ;
#18197=ORIENTED_EDGE ( 'NONE', *, *, #18292, .F. ) ;
#18209=ORIENTED_EDGE ( 'NONE', *, *, #13664, .T. ) ;
#18217=LINE ( 'NONE', #9727, #3532 ) ;
#18220=CIRCLE ( 'NONE', #18570, 0.3000000000000016542 ) ;
#18228=CARTESIAN_POINT ( 'NONE',  ( 33.19999999999999574, 85.00000000000000000, 78.20000000000000284 ) ) ;
#18241=DIRECTION ( 'NONE',  ( 0.000000000000000000, 0.000000000000000000, -1.000000000000000000 ) ) ;
#18246=CARTESIAN_POINT ( 'NONE',  ( -34.70000000000001705, 85.00000000000000000, 79.39999999999999147 ) ) ;
#18256=ORIENTED_EDGE ( 'NONE', *, *, #5270, .T. ) ;
#18259=EDGE_LOOP ( 'NONE', ( #14236, #2836, #8314, #7150 ) ) ;
#18270=AXIS2_PLACEMENT_3D ( 'NONE', #20764, #17501, #17935 ) ;
#18271=CARTESIAN_POINT ( 'NONE',  ( 33.19999999999999574, 84.70000000000001705, 78.50000000000000000 ) ) ;
#18278=ORIENTED_EDGE ( 'NONE', *, *, #21020, .F. ) ;
#18285=DIRECTION ( 'NONE',  ( 0.000000000000000000, 0.000000000000000000, -1.000000000000000000 ) ) ;
#18292=EDGE_CURVE ( 'NONE', #3127, #13680, #15326, .T. ) ;
#18305=EDGE_LOOP ( 'NONE', ( #11443, #11013, #3457, #19267 ) ) ;
#18323=DIRECTION ( 'NONE',  ( 0.000000000000000000, 0.000000000000000000, -1.000000000000000000 ) ) ;
#18327=PLANE ( 'NONE',  #13517 ) ;
#18332=EDGE_LOOP ( 'NONE', ( #20114, #14303, #14048, #14550 ) ) ;
#18334=CARTESIAN_POINT ( 'NONE',  ( -33.20000000000001705, 84.70000000000001705, 78.79999999999999716 ) ) ;
#18345=CARTESIAN_POINT ( 'NONE',  ( -34.39999999999999858, 84.70000000000001705, 0.6000000000000033085 ) ) ;
#18347=DIRECTION ( 'NONE',  ( 0.000000000000000000, 0.000000000000000000, -1.000000000000000000 ) ) ;
#18358=CARTESIAN_POINT ( 'NONE',  ( -33.80000000000000426, -84.70000000000001705, -5.863365348801607979E-15 ) ) ;
#18363=ORIENTED_EDGE ( 'NONE', *, *, #15510, .F. ) ;
#18369=CARTESIAN_POINT ( 'NONE',  ( -33.20000000000000284, 84.70000000000001705, 1.500000000000000222 ) ) ;
#18397=CARTESIAN_POINT ( 'NONE',  ( 30.19999999999999574, 70.00000000000000000, 1.200000000000003064 ) ) ;
#18401=AXIS2_PLACEMENT_3D ( 'NONE', #12590, #10823, #2309 ) ;
#18408=ORIENTED_EDGE ( 'NONE', *, *, #8567, .F. ) ;
#18419=AXIS2_PLACEMENT_3D ( 'NONE', #14450, #813, #2846 ) ;
#18420=AXIS2_PLACEMENT_3D ( 'NONE', #2969, #4320, #11566 ) ;
#18428=LINE ( 'NONE', #3110, #19595 ) ;
#18430=CARTESIAN_POINT ( 'NONE',  ( 30.49999999999999645, -123.9599366953518711, 10.00000000000000178 ) ) ;
#18445=DIRECTION ( 'NONE',  ( 1.000000000000000000, 0.000000000000000000, 6.123233995736764803E-17 ) ) ;
#18452=CARTESIAN_POINT ( 'NONE',  ( 30.19999999999999574, 69.70000000000000284, 4.011548038196366406E-15 ) ) ;
#18462=CIRCLE ( 'NONE', #7053, 0.6000000000000000888 ) ;
#18478=VECTOR ( 'NONE', #5259, 1000.000000000000000 ) ;
#18480=ORIENTED_EDGE ( 'NONE', *, *, #8859, .T. ) ;
#18514=DIRECTION ( 'NONE',  ( 0.000000000000000000, 0.000000000000000000, -1.000000000000000000 ) ) ;
#18522=ADVANCED_FACE ( 'NONE', ( #9937 ), #9481, .T. ) ;
#18540=DIRECTION ( 'NONE',  ( -0.000000000000000000, -3.614007241618412274E-15, -1.000000000000000000 ) ) ;
#18568=DIRECTION ( 'NONE',  ( 1.000000000000000000, -0.000000000000000000, 1.734723475976806848E-16 ) ) ;
#18570=AXIS2_PLACEMENT_3D ( 'NONE', #13494, #20334, #5680 ) ;
#18582=ORIENTED_EDGE ( 'NONE', *, *, #18835, .F. ) ;
#18603=DIRECTION ( 'NONE',  ( -1.000000000000000000, 0.000000000000000000, 0.000000000000000000 ) ) ;
#18604=DIRECTION ( 'NONE',  ( 1.000000000000000000, -0.000000000000000000, 6.123233995736764803E-17 ) ) ;
#18615=EDGE_CURVE ( 'NONE', #18983, #1780, #3665, .T. ) ;
#18616=DIRECTION ( 'NONE',  ( 0.000000000000000000, 0.000000000000000000, 1.000000000000000000 ) ) ;
#18624=ORIENTED_EDGE ( 'NONE', *, *, #10406, .T. ) ;
#18638=CARTESIAN_POINT ( 'NONE',  ( -7.347880794884131322E-17, -84.70000000000001705, 1.200000000000002176 ) ) ;
#18654=CARTESIAN_POINT ( 'NONE',  ( -30.19999999999999574, 70.00000000000000000, 0.2999999999999996558 ) ) ;
#18657=ORIENTED_EDGE ( 'NONE', *, *, #21179, .T. ) ;
#18665=LINE ( 'NONE', #3448, #19132 ) ;
#18674=CIRCLE ( 'NONE', #1112, 0.6000000000000033085 ) ;
#18735=LINE ( 'NONE', #1730, #9873 ) ;
#18736=ORIENTED_EDGE ( 'NONE', *, *, #21806, .T. ) ;
#18740=FILL_AREA_STYLE ('',( #263 ) ) ;
#18741=ORIENTED_EDGE ( 'NONE', *, *, #12768, .F. ) ;
#18751=CIRCLE ( 'NONE', #20551, 0.2999999999999947153 ) ;
#18757=ORIENTED_EDGE ( 'NONE', *, *, #20507, .T. ) ;
#18765=CARTESIAN_POINT ( 'NONE',  ( 34.39999999999998437, 84.70000000000001705, 79.39999999999999147 ) ) ;
#18773=DIRECTION ( 'NONE',  ( -1.445602896647331422E-15, 0.000000000000000000, -1.000000000000000000 ) ) ;
#18777=ORIENTED_EDGE ( 'NONE', *, *, #20467, .T. ) ;
#18814=EDGE_CURVE ( 'NONE', #15951, #18912, #11026, .T. ) ;
#18820=DIRECTION ( 'NONE',  ( -0.000000000000000000, 1.000000000000000000, -0.000000000000000000 ) ) ;
#18835=EDGE_CURVE ( 'NONE', #22033, #5083, #19230, .T. ) ;
#18859=DIRECTION ( 'NONE',  ( 0.000000000000000000, 0.000000000000000000, -1.000000000000000000 ) ) ;
#18862=DIRECTION ( 'NONE',  ( 1.734723475976806848E-16, 0.000000000000000000, -1.000000000000000000 ) ) ;
#18864=DIRECTION ( 'NONE',  ( 1.000000000000000000, 0.000000000000000000, 0.000000000000000000 ) ) ;
#18874=AXIS2_PLACEMENT_3D ( 'NONE', #18358, #7871, #11305 ) ;
#18891=AXIS2_PLACEMENT_3D ( 'NONE', #19874, #4539, #18190 ) ;
#18912=VERTEX_POINT ( 'NONE', #2863 ) ;
#18921=TOROIDAL_SURFACE ( 'NONE', #6774, 0.5999999999999999778, 0.2999999999999999889 ) ;
#18953=ORIENTED_EDGE ( 'NONE', *, *, #9663, .T. ) ;
#18963=LINE ( 'NONE', #13783, #23 ) ;
#18982=ORIENTED_EDGE ( 'NONE', *, *, #9967, .F. ) ;
#18983=VERTEX_POINT ( 'NONE', #14928 ) ;
#18987=ADVANCED_FACE ( 'NONE', ( #21781 ), #150, .F. ) ;
#19010=CARTESIAN_POINT ( 'NONE',  ( -35.00000000000001421, 85.00000000000000000, 78.50000000000000000 ) ) ;
#19016=ORIENTED_EDGE ( 'NONE', *, *, #6782, .T. ) ;
#19018=CIRCLE ( 'NONE', #4719, 0.3000000000000016542 ) ;
#19023=TOROIDAL_SURFACE ( 'NONE', #9369, 0.2999999999999999889, 0.2999999999999999889 ) ;
#19027=UNCERTAINTY_MEASURE_WITH_UNIT (LENGTH_MEASURE( 1.000000000000000082E-05 ), #3960, 'distance_accuracy_value', 'NONE');
#19036=STYLED_ITEM ( 'NONE', ( #17271 ), #13188 ) ;
#19038=ORIENTED_EDGE ( 'NONE', *, *, #15726, .F. ) ;
#19041=ADVANCED_FACE ( 'NONE', ( #12116 ), #15145, .T. ) ;
#19108=ORIENTED_EDGE ( 'NONE', *, *, #8859, .F. ) ;
#19109=LINE ( 'NONE', #20386, #13025 ) ;
#19128=EDGE_CURVE ( 'NONE', #21291, #21163, #6344, .T. ) ;
#19132=VECTOR ( 'NONE', #15419, 1000.000000000000000 ) ;
#19141=EDGE_CURVE ( 'NONE', #3486, #9143, #20756, .T. ) ;
#19148=EDGE_LOOP ( 'NONE', ( #14369, #2874, #21710, #9916 ) ) ;
#19166=CARTESIAN_POINT ( 'NONE',  ( -30.79999999999999005, 85.00000000000000000, 2.571758278209449353E-16 ) ) ;
#19179=EDGE_CURVE ( 'NONE', #6175, #8145, #9601, .T. ) ;
#19202=ORIENTED_EDGE ( 'NONE', *, *, #6815, .T. ) ;
#19205=DIRECTION ( 'NONE',  ( -6.123233995736764803E-17, 0.000000000000000000, 1.000000000000000000 ) ) ;
#19226=LINE ( 'NONE', #17540, #5961 ) ;
#19230=CIRCLE ( 'NONE', #3864, 0.5999999999999998668 ) ;
#19233=ADVANCED_FACE ( 'NONE', ( #9097 ), #5536, .F. ) ;
#19267=ORIENTED_EDGE ( 'NONE', *, *, #731, .F. ) ;
#19284=ORIENTED_EDGE ( 'NONE', *, *, #4944, .F. ) ;
#19290=CIRCLE ( 'NONE', #5738, 0.2999999999999947153 ) ;
#19292=AXIS2_PLACEMENT_3D ( 'NONE', #20880, #15496, #1859 ) ;
#19322=ORIENTED_EDGE ( 'NONE', *, *, #4944, .T. ) ;
#19326=TOROIDAL_SURFACE ( 'NONE', #9688, 0.2999999999999999889, 0.2999999999999999889 ) ;
#19332=EDGE_LOOP ( 'NONE', ( #21256, #8164, #1044, #14395 ) ) ;
#19368=VECTOR ( 'NONE', #1666, 1000.000000000000000 ) ;
#19373=ORIENTED_EDGE ( 'NONE', *, *, #20643, .T. ) ;
#19374=PLANE ( 'NONE',  #10031 ) ;
#19378=CARTESIAN_POINT ( 'NONE',  ( 33.19999999999999574, 84.70000000000001705, 1.500000000000004219 ) ) ;
#19396=ORIENTED_EDGE ( 'NONE', *, *, #5124, .T. ) ;
#19413=VERTEX_POINT ( 'NONE', #18369 ) ;
#19416=( GEOMETRIC_REPRESENTATION_CONTEXT ( 3 ) GLOBAL_UNCERTAINTY_ASSIGNED_CONTEXT ( ( #15645 ) ) GLOBAL_UNIT_ASSIGNED_CONTEXT ( ( #12874, #6300, #1353 ) ) REPRESENTATION_CONTEXT ( 'NONE', 'WORKASPACE' ) );
#19418=DIRECTION ( 'NONE',  ( 1.000000000000000000, -0.000000000000000000, 0.000000000000000000 ) ) ;
#19431=ADVANCED_FACE ( 'NONE', ( #17141 ), #3277, .T. ) ;
#19453=ADVANCED_FACE ( 'NONE', ( #15121 ), #21968, .T. ) ;
#19464=ORIENTED_EDGE ( 'NONE', *, *, #4413, .F. ) ;
#19465=EDGE_CURVE ( 'NONE', #823, #1780, #4916, .T. ) ;
#19468=DIRECTION ( 'NONE',  ( -0.000000000000000000, 0.000000000000000000, 1.000000000000000000 ) ) ;
#19476=EDGE_CURVE ( 'NONE', #17830, #6583, #15608, .T. ) ;
#19479=DIRECTION ( 'NONE',  ( 1.000000000000000000, -0.000000000000000000, 6.123233995736764803E-17 ) ) ;
#19490=VECTOR ( 'NONE', #12802, 1000.000000000000000 ) ;
#19518=AXIS2_PLACEMENT_3D ( 'NONE', #19010, #15949, #17307 ) ;
#19551=ORIENTED_EDGE ( 'NONE', *, *, #10892, .F. ) ;
#19553=ORIENTED_EDGE ( 'NONE', *, *, #5906, .T. ) ;
#19555=AXIS2_PLACEMENT_3D ( 'NONE', #537, #10846, #662 ) ;
#19568=DIRECTION ( 'NONE',  ( 0.000000000000000000, 0.000000000000000000, -1.000000000000000000 ) ) ;
#19581=AXIS2_PLACEMENT_3D ( 'NONE', #2933, #6420, #9760 ) ;
#19589=DIRECTION ( 'NONE',  ( 0.000000000000000000, 0.000000000000000000, -1.000000000000000000 ) ) ;
#19595=VECTOR ( 'NONE', #9944, 1000.000000000000000 ) ;
#19596=AXIS2_PLACEMENT_3D ( 'NONE', #13977, #17335, #12185 ) ;
#19598=CIRCLE ( 'NONE', #10655, 0.3000000000000016542 ) ;
#19629=CARTESIAN_POINT ( 'NONE',  ( -7.347880794884131322E-17, -85.00000000000000000, 1.200000000000002176 ) ) ;
#19637=PLANE ( 'NONE',  #17357 ) ;
#19642=EDGE_CURVE ( 'NONE', #4505, #21013, #15572, .T. ) ;
#19650=LINE ( 'NONE', #6125, #4852 ) ;
#19666=ORIENTED_EDGE ( 'NONE', *, *, #731, .T. ) ;
#19683=LINE ( 'NONE', #3716, #652 ) ;
#19724=VERTEX_POINT ( 'NONE', #7859 ) ;
#19767=ORIENTED_EDGE ( 'NONE', *, *, #15757, .T. ) ;
#19769=LINE ( 'NONE', #18195, #16089 ) ;
#19778=DIRECTION ( 'NONE',  ( -0.000000000000000000, -0.000000000000000000, -1.000000000000000000 ) ) ;
#19783=ORIENTED_EDGE ( 'NONE', *, *, #17881, .F. ) ;
#19793=CARTESIAN_POINT ( 'NONE',  ( -33.50000000000000000, -84.70000000000001705, 1.800000000000000266 ) ) ;
#19797=CARTESIAN_POINT ( 'NONE',  ( -34.39999999999999858, 85.00000000000000000, 0.6000000000000033085 ) ) ;
#19801=EDGE_CURVE ( 'NONE', #11049, #15362, #4097, .T. ) ;
#19810=CARTESIAN_POINT ( 'NONE',  ( 33.49999999999999289, 84.70000000000001705, 1.500000000000001332 ) ) ;
#19817=CARTESIAN_POINT ( 'NONE',  ( 33.19999999999999574, 85.00000000000000000, 1.200000000000004174 ) ) ;
#19819=DIRECTION ( 'NONE',  ( 0.000000000000000000, 0.000000000000000000, -1.000000000000000000 ) ) ;
#19821=DIRECTION ( 'NONE',  ( 0.000000000000000000, 0.000000000000000000, 1.000000000000000000 ) ) ;
#19822=CIRCLE ( 'NONE', #509, 0.2999999999999999334 ) ;
#19825=DIRECTION ( 'NONE',  ( -0.000000000000000000, -0.000000000000000000, -1.000000000000000000 ) ) ;
#19848=CARTESIAN_POINT ( 'NONE',  ( -33.50000000000001421, -84.70000000000001705, 80.00000000000000000 ) ) ;
#19865=DIRECTION ( 'NONE',  ( -1.000000000000000000, -0.000000000000000000, -6.123233995736764803E-17 ) ) ;
#19874=CARTESIAN_POINT ( 'NONE',  ( 33.19999999999999574, -84.70000000000001705, 78.20000000000000284 ) ) ;
#19888=AXIS2_PLACEMENT_3D ( 'NONE', #17579, #18820, #2245 ) ;
#19912=ORIENTED_EDGE ( 'NONE', *, *, #18814, .T. ) ;
#19915=DIRECTION ( 'NONE',  ( -0.000000000000000000, 1.000000000000000000, -0.000000000000000000 ) ) ;
#19923=CIRCLE ( 'NONE', #12036, 0.5999999999999998668 ) ;
#19938=CARTESIAN_POINT ( 'NONE',  ( 34.39999999999998437, -84.70000000000001705, 79.70000000000000284 ) ) ;
#19942=DIRECTION ( 'NONE',  ( 0.000000000000000000, 0.000000000000000000, -1.000000000000000000 ) ) ;
#19943=DIRECTION ( 'NONE',  ( -0.000000000000000000, 1.000000000000000000, -0.000000000000000000 ) ) ;
#19963=EDGE_CURVE ( 'NONE', #12088, #4692, #18462, .T. ) ;
#19975=ORIENTED_EDGE ( 'NONE', *, *, #9612, .T. ) ;
#19986=FACE_OUTER_BOUND ( 'NONE', #16877, .T. ) ;
#19988=DIRECTION ( 'NONE',  ( -0.000000000000000000, -1.000000000000000000, 0.000000000000000000 ) ) ;
#19993=DIRECTION ( 'NONE',  ( 1.000000000000000000, -0.000000000000000000, 6.123233995736764803E-17 ) ) ;
#19996=DIRECTION ( 'NONE',  ( 0.000000000000000000, 0.000000000000000000, -1.000000000000000000 ) ) ;
#20000=EDGE_LOOP ( 'NONE', ( #14031, #3248, #18363, #18145 ) ) ;
#20002=DIRECTION ( 'NONE',  ( 1.000000000000000000, 0.000000000000000000, 6.123233995736764803E-17 ) ) ;
#20006=CARTESIAN_POINT ( 'NONE',  ( 30.79999999999999716, 69.70000000000000284, 1.200000000000003064 ) ) ;
#20009=EDGE_LOOP ( 'NONE', ( #20118, #13637, #14337, #15276 ) ) ;
#20030=CARTESIAN_POINT ( 'NONE',  ( -34.70000000000001705, -84.70000000000001705, 80.00000000000000000 ) ) ;
#20032=ORIENTED_EDGE ( 'NONE', *, *, #2901, .F. ) ;
#20041=VECTOR ( 'NONE', #9213, 1000.000000000000000 ) ;
#20114=ORIENTED_EDGE ( 'NONE', *, *, #20490, .T. ) ;
#20118=ORIENTED_EDGE ( 'NONE', *, *, #865, .T. ) ;
#20137=DIRECTION ( 'NONE',  ( -6.123233995736764803E-17, 0.000000000000000000, 1.000000000000000000 ) ) ;
#20145=COLOUR_RGB ( '', 0.40784314, 0.44705882, 0.49803922) ;
#20170=CARTESIAN_POINT ( 'NONE',  ( 33.19999999999999574, -84.70000000000001705, 1.500000000000004219 ) ) ;
#20184=ORIENTED_EDGE ( 'NONE', *, *, #7705, .F. ) ;
#20206=ORIENTED_EDGE ( 'NONE', *, *, #3235, .F. ) ;
#20222=CIRCLE ( 'NONE', #18420, 0.2999999999999999334 ) ;
#20227=DIRECTION ( 'NONE',  ( 1.000000000000000000, 0.000000000000000000, 0.000000000000000000 ) ) ;
#20230=DIRECTION ( 'NONE',  ( -0.000000000000000000, 1.000000000000000000, -0.000000000000000000 ) ) ;
#20271=ORIENTED_EDGE ( 'NONE', *, *, #20574, .T. ) ;
#20272=DIRECTION ( 'NONE',  ( -1.000000000000000000, -0.000000000000000000, -0.000000000000000000 ) ) ;
#20282=DIRECTION ( 'NONE',  ( 6.123233995736764803E-17, 0.000000000000000000, -1.000000000000000000 ) ) ;
#20285=VECTOR ( 'NONE', #713, 1000.000000000000000 ) ;
#20299=EDGE_CURVE ( 'NONE', #16703, #12463, #2497, .T. ) ;
#20310=DIRECTION ( 'NONE',  ( -1.000000000000000000, 1.788744114411106313E-17, -6.123233995736764803E-17 ) ) ;
#20313=ORIENTED_EDGE ( 'NONE', *, *, #9739, .T. ) ;
#20326=VERTEX_POINT ( 'NONE', #10885 ) ;
#20330=VERTEX_POINT ( 'NONE', #369 ) ;
#20334=DIRECTION ( 'NONE',  ( 0.000000000000000000, 0.000000000000000000, -1.000000000000000000 ) ) ;
#20338=FACE_OUTER_BOUND ( 'NONE', #1629, .T. ) ;
#20355=DIRECTION ( 'NONE',  ( 0.000000000000000000, 1.000000000000000000, -1.084202172485523564E-15 ) ) ;
#20356=DIRECTION ( 'NONE',  ( -1.000000000000000000, 0.000000000000000000, -8.673617379884034239E-17 ) ) ;
#20361=FACE_OUTER_BOUND ( 'NONE', #11482, .T. ) ;
#20374=DIRECTION ( 'NONE',  ( 6.123233995736764803E-17, 0.000000000000000000, -1.000000000000000000 ) ) ;
#20386=CARTESIAN_POINT ( 'NONE',  ( 30.50000000000000000, -84.70000000000001705, 4.011548038196366406E-15 ) ) ;
#20387=AXIS2_PLACEMENT_3D ( 'NONE', #11126, #19988, #9691 ) ;
#20396=PRODUCT_CONTEXT ( 'NONE', #17584, 'mechanical' ) ;
#20404=AXIS2_PLACEMENT_3D ( 'NONE', #21867, #15026, #3282 ) ;
#20416=EDGE_LOOP ( 'NONE', ( #14212, #8906, #21214, #16839 ) ) ;
#20449=DIRECTION ( 'NONE',  ( 0.000000000000000000, 1.000000000000000000, 0.000000000000000000 ) ) ;
#20450=CIRCLE ( 'NONE', #18270, 0.3000000000000016542 ) ;
#20460=FACE_OUTER_BOUND ( 'NONE', #18305, .T. ) ;
#20467=EDGE_CURVE ( 'NONE', #1975, #9891, #15373, .T. ) ;
#20473=DIRECTION ( 'NONE',  ( 1.000000000000000000, -0.000000000000000000, 6.123233995736764803E-17 ) ) ;
#20475=DIRECTION ( 'NONE',  ( -0.000000000000000000, 1.000000000000000000, -0.000000000000000000 ) ) ;
#20485=ORIENTED_EDGE ( 'NONE', *, *, #1135, .T. ) ;
#20488=CARTESIAN_POINT ( 'NONE',  ( -34.40000000000001279, -85.00000000000000000, 79.39999999999999147 ) ) ;
#20490=EDGE_CURVE ( 'NONE', #17432, #6971, #14311, .T. ) ;
#20507=EDGE_CURVE ( 'NONE', #8082, #21431, #15237, .T. ) ;
#20534=DIRECTION ( 'NONE',  ( 1.788744114411106313E-17, 1.000000000000000000, 1.095289877103613968E-33 ) ) ;
#20543=CARTESIAN_POINT ( 'NONE',  ( 33.19999999999999574, -84.70000000000001705, 78.79999999999999716 ) ) ;
#20548=ADVANCED_FACE ( 'NONE', ( #5182 ), #6767, .F. ) ;
#20551=AXIS2_PLACEMENT_3D ( 'NONE', #456, #15558, #8980 ) ;
#20557=VERTEX_POINT ( 'NONE', #10336 ) ;
#20561=DIRECTION ( 'NONE',  ( -1.000000000000000000, -0.000000000000000000, -0.000000000000000000 ) ) ;
#20563=DIRECTION ( 'NONE',  ( -0.000000000000000000, 0.000000000000000000, -1.000000000000000000 ) ) ;
#20564=VECTOR ( 'NONE', #20473, 1000.000000000000000 ) ;
#20565=CARTESIAN_POINT ( 'NONE',  ( -33.20000000000001705, -84.70000000000001705, 78.79999999999999716 ) ) ;
#20571=DIRECTION ( 'NONE',  ( -1.000000000000000000, 0.000000000000000000, 1.445602896647331225E-15 ) ) ;
#20572=ORIENTED_EDGE ( 'NONE', *, *, #19141, .T. ) ;
#20574=EDGE_CURVE ( 'NONE', #3156, #20557, #13602, .T. ) ;
#20591=TOROIDAL_SURFACE ( 'NONE', #2376, 0.5999999999999999778, 0.2999999999999999889 ) ;
#20609=EDGE_LOOP ( 'NONE', ( #5735, #18408, #19038, #123 ) ) ;
#20613=ORIENTED_EDGE ( 'NONE', *, *, #825, .T. ) ;
#20618=ORIENTED_EDGE ( 'NONE', *, *, #19801, .F. ) ;
#20619=DIRECTION ( 'NONE',  ( 8.673617379884034239E-17, 0.000000000000000000, -1.000000000000000000 ) ) ;
#20628=LINE ( 'NONE', #353, #15176 ) ;
#20635=CARTESIAN_POINT ( 'NONE',  ( 30.49999999999999645, -84.70000000000001705, 1.200000000000003064 ) ) ;
#20637=CARTESIAN_POINT ( 'NONE',  ( -30.49999999999998934, 69.70000000000001705, 1.199999999999999734 ) ) ;
#20643=EDGE_CURVE ( 'NONE', #445, #3156, #8869, .T. ) ;
#20648=DIRECTION ( 'NONE',  ( 1.000000000000000000, 0.000000000000000000, -0.000000000000000000 ) ) ;
#20667=ORIENTED_EDGE ( 'NONE', *, *, #17617, .F. ) ;
#20684=VERTEX_POINT ( 'NONE', #19378 ) ;
#20689=DIRECTION ( 'NONE',  ( 1.788744114411106313E-17, 1.000000000000000000, 1.095289877103613968E-33 ) ) ;
#20692=EDGE_CURVE ( 'NONE', #8060, #15052, #3613, .T. ) ;
#20694=CARTESIAN_POINT ( 'NONE',  ( -34.40000000000001279, 84.70000000000001705, 79.70000000000000284 ) ) ;
#20717=ORIENTED_EDGE ( 'NONE', *, *, #6958, .F. ) ;
#20728=ORIENTED_EDGE ( 'NONE', *, *, #5563, .T. ) ;
#20755=VECTOR ( 'NONE', #15675, 1000.000000000000000 ) ;
#20756=LINE ( 'NONE', #17263, #16308 ) ;
#20762=ADVANCED_FACE ( 'NONE', ( #18012 ), #19326, .T. ) ;
#20764=CARTESIAN_POINT ( 'NONE',  ( 34.69999999999998863, 84.70000000000001705, 79.39999999999999147 ) ) ;
#20765=CARTESIAN_POINT ( 'NONE',  ( 33.19999999999999574, -84.70000000000001705, 1.799999999999996048 ) ) ;
#20769=CARTESIAN_POINT ( 'NONE',  ( 33.79999999999999716, -85.00000000000000000, 1.799999999999996048 ) ) ;
#20774=DIRECTION ( 'NONE',  ( 0.000000000000000000, 1.000000000000000000, 0.000000000000000000 ) ) ;
#20795=DIRECTION ( 'NONE',  ( -1.000000000000000000, 0.000000000000000000, 0.000000000000000000 ) ) ;
#20801=DIRECTION ( 'NONE',  ( -1.000000000000000000, 0.000000000000000000, 0.000000000000000000 ) ) ;
#20803=DIRECTION ( 'NONE',  ( 0.000000000000000000, 0.000000000000000000, -1.000000000000000000 ) ) ;
#20823=CARTESIAN_POINT ( 'NONE',  ( -30.79999999999999361, -84.70000000000001705, 1.200000000000000622 ) ) ;
#20830=ORIENTED_EDGE ( 'NONE', *, *, #18814, .F. ) ;
#20839=EDGE_LOOP ( 'NONE', ( #20613, #17399, #8327, #18197 ) ) ;
#20845=DIRECTION ( 'NONE',  ( 0.000000000000000000, 0.000000000000000000, -1.000000000000000000 ) ) ;
#20859=EDGE_CURVE ( 'NONE', #21689, #15362, #17548, .T. ) ;
#20861=CARTESIAN_POINT ( 'NONE',  ( 33.19999999999999574, -85.00000000000000000, 1.799999999999996048 ) ) ;
#20876=ORIENTED_EDGE ( 'NONE', *, *, #14595, .T. ) ;
#20880=CARTESIAN_POINT ( 'NONE',  ( -34.70000000000000284, 84.70000000000001705, 0.6000000000000033085 ) ) ;
#20882=AXIS2_PLACEMENT_3D ( 'NONE', #12970, #19943, #19819 ) ;
#20883=CARTESIAN_POINT ( 'NONE',  ( 30.49999999999999645, -84.70000000000001705, 0.3000000000000033751 ) ) ;
#20886=EDGE_LOOP ( 'NONE', ( #14834, #12915, #5882, #13380 ) ) ;
#20952=VECTOR ( 'NONE', #19865, 1000.000000000000000 ) ;
#20962=AXIS2_PLACEMENT_3D ( 'NONE', #14468, #7347, #722 ) ;
#20965=TOROIDAL_SURFACE ( 'NONE', #17725, 0.5999999999999999778, 0.2999999999999999889 ) ;
#20984=ORIENTED_EDGE ( 'NONE', *, *, #11674, .F. ) ;
#20999=ORIENTED_EDGE ( 'NONE', *, *, #1580, .T. ) ;
#21001=FACE_OUTER_BOUND ( 'NONE', #5861, .T. ) ;
#21005=DIRECTION ( 'NONE',  ( -0.000000000000000000, 1.000000000000000000, -0.000000000000000000 ) ) ;
#21013=VERTEX_POINT ( 'NONE', #12825 ) ;
#21020=EDGE_CURVE ( 'NONE', #2890, #11049, #16417, .T. ) ;
#21051=CIRCLE ( 'NONE', #16747, 0.2999999999999999889 ) ;
#21052=ADVANCED_FACE ( 'NONE', ( #18085 ), #7827, .T. ) ;
#21071=DIRECTION ( 'NONE',  ( 0.000000000000000000, 0.000000000000000000, -1.000000000000000000 ) ) ;
#21087=VERTEX_POINT ( 'NONE', #856 ) ;
#21092=AXIS2_PLACEMENT_3D ( 'NONE', #22140, #4888, #6690 ) ;
#21115=ORIENTED_EDGE ( 'NONE', *, *, #11066, .T. ) ;
#21117=FACE_OUTER_BOUND ( 'NONE', #15689, .T. ) ;
#21129=LINE ( 'NONE', #15834, #10861 ) ;
#21137=EDGE_LOOP ( 'NONE', ( #14102, #7904, #13709, #1685 ) ) ;
#21144=EDGE_CURVE ( 'NONE', #21013, #10999, #6697, .T. ) ;
#21158=CARTESIAN_POINT ( 'NONE',  ( -30.79999999999999361, -84.70000000000001705, 0.3000000000000002665 ) ) ;
#21159=DIRECTION ( 'NONE',  ( 0.000000000000000000, 0.000000000000000000, 1.000000000000000000 ) ) ;
#21163=VERTEX_POINT ( 'NONE', #5122 ) ;
#21170=ORIENTED_EDGE ( 'NONE', *, *, #1073, .T. ) ;
#21179=EDGE_CURVE ( 'NONE', #15951, #17181, #4344, .T. ) ;
#21214=ORIENTED_EDGE ( 'NONE', *, *, #4685, .F. ) ;
#21215=LINE ( 'NONE', #8907, #3852 ) ;
#21229=CARTESIAN_POINT ( 'NONE',  ( -35.00000000000001421, -84.70000000000001705, 79.39999999999999147 ) ) ;
#21255=DIRECTION ( 'NONE',  ( 6.123233995736764803E-17, 0.000000000000000000, -1.000000000000000000 ) ) ;
#21256=ORIENTED_EDGE ( 'NONE', *, *, #2550, .T. ) ;
#21291=VERTEX_POINT ( 'NONE', #9121 ) ;
#21293=ADVANCED_FACE ( 'NONE', ( #13932, #7572 ), #7243, .F. ) ;
#21294=FILL_AREA_STYLE_COLOUR ( '', #20145 ) ;
#21305=ORIENTED_EDGE ( 'NONE', *, *, #16107, .F. ) ;
#21312=VECTOR ( 'NONE', #2505, 1000.000000000000000 ) ;
#21317=ORIENTED_EDGE ( 'NONE', *, *, #1972, .T. ) ;
#21352=AXIS2_PLACEMENT_3D ( 'NONE', #10476, #5346, #8354 ) ;
#21356=ORIENTED_EDGE ( 'NONE', *, *, #11674, .T. ) ;
#21357=AXIS2_PLACEMENT_3D ( 'NONE', #17473, #2356, #21071 ) ;
#21365=CARTESIAN_POINT ( 'NONE',  ( 30.19999999999999574, 69.70000000000000284, 1.200000000000003064 ) ) ;
#21371=LINE ( 'NONE', #17987, #10617 ) ;
#21391=FACE_OUTER_BOUND ( 'NONE', #18259, .T. ) ;
#21401=VECTOR ( 'NONE', #6718, 1000.000000000000000 ) ;
#21406=EDGE_CURVE ( 'NONE', #21087, #12623, #12846, .T. ) ;
#21413=FACE_OUTER_BOUND ( 'NONE', #11337, .T. ) ;
#21431=VERTEX_POINT ( 'NONE', #1160 ) ;
#21434=ORIENTED_EDGE ( 'NONE', *, *, #4528, .F. ) ;
#21454=CARTESIAN_POINT ( 'NONE',  ( 33.19999999999999574, 85.00000000000000000, 78.79999999999999716 ) ) ;
#21476=EDGE_CURVE ( 'NONE', #16703, #17181, #7881, .T. ) ;
#21482=CARTESIAN_POINT ( 'NONE',  ( 34.39999999999998437, 85.00000000000000000, 0.6000000000000041966 ) ) ;
#21488=DIRECTION ( 'NONE',  ( 0.000000000000000000, 0.000000000000000000, 1.000000000000000000 ) ) ;
#21496=DIRECTION ( 'NONE',  ( 0.000000000000000000, 0.000000000000000000, -1.000000000000000000 ) ) ;
#21505=DIRECTION ( 'NONE',  ( 1.000000000000000000, 0.000000000000000000, 0.000000000000000000 ) ) ;
#21507=PLANE ( 'NONE',  #4900 ) ;
#21513=AXIS2_PLACEMENT_3D ( 'NONE', #10483, #14042, #3883 ) ;
#21516=DIRECTION ( 'NONE',  ( 1.734723475976806848E-16, 0.000000000000000000, -1.000000000000000000 ) ) ;
#21521=AXIS2_PLACEMENT_3D ( 'NONE', #3862, #12324, #7329 ) ;
#21569=EDGE_CURVE ( 'NONE', #15018, #9891, #1087, .T. ) ;
#21595=DIRECTION ( 'NONE',  ( 8.673617379884034239E-17, 0.000000000000000000, -1.000000000000000000 ) ) ;
#21607=AXIS2_PLACEMENT_3D ( 'NONE', #7583, #12683, #2635 ) ;
#21616=CARTESIAN_POINT ( 'NONE',  ( -35.00000000000001421, 85.00000000000000000, 80.00000000000000000 ) ) ;
#21664=AXIS2_PLACEMENT_3D ( 'NONE', #5849, #14324, #17794 ) ;
#21666=DIRECTION ( 'NONE',  ( 0.000000000000000000, 0.000000000000000000, -1.000000000000000000 ) ) ;
#21672=ADVANCED_FACE ( 'NONE', ( #47 ), #19374, .T. ) ;
#21685=CIRCLE ( 'NONE', #5252, 0.5999999999999999778 ) ;
#21689=VERTEX_POINT ( 'NONE', #146 ) ;
#21697=CIRCLE ( 'NONE', #10601, 0.2999999999999999334 ) ;
#21710=ORIENTED_EDGE ( 'NONE', *, *, #20467, .F. ) ;
#21723=EDGE_CURVE ( 'NONE', #9996, #21689, #6843, .T. ) ;
#21750=ORIENTED_EDGE ( 'NONE', *, *, #7127, .T. ) ;
#21751=ADVANCED_FACE ( 'NONE', ( #21391 ), #9184, .T. ) ;
#21754=EDGE_LOOP ( 'NONE', ( #17598, #10344, #17516, #11919 ) ) ;
#21769=DIRECTION ( 'NONE',  ( 1.000000000000000000, 0.000000000000000000, 6.123233995736764803E-17 ) ) ;
#21781=FACE_OUTER_BOUND ( 'NONE', #248, .T. ) ;
#21785=DIRECTION ( 'NONE',  ( 0.000000000000000000, -1.000000000000000000, 0.000000000000000000 ) ) ;
#21786=FACE_OUTER_BOUND ( 'NONE', #11449, .T. ) ;
#21805=EDGE_CURVE ( 'NONE', #15362, #5205, #18963, .T. ) ;
#21806=EDGE_CURVE ( 'NONE', #2890, #15663, #2878, .T. ) ;
#21819=ORIENTED_EDGE ( 'NONE', *, *, #3347, .F. ) ;
#21859=ORIENTED_EDGE ( 'NONE', *, *, #16950, .T. ) ;
#21867=CARTESIAN_POINT ( 'NONE',  ( -30.79999999999999361, -84.70000000000001705, 1.199999999999999734 ) ) ;
#21876=ORIENTED_EDGE ( 'NONE', *, *, #6480, .F. ) ;
#21886=AXIS2_PLACEMENT_3D ( 'NONE', #11495, #6155, #18323 ) ;
#21895=DIRECTION ( 'NONE',  ( -0.000000000000000000, -1.000000000000000000, -0.000000000000000000 ) ) ;
#21903=DIRECTION ( 'NONE',  ( 0.000000000000000000, 1.000000000000000000, -0.000000000000000000 ) ) ;
#21915=CARTESIAN_POINT ( 'NONE',  ( 30.79999999999999716, -84.70000000000001705, 1.200000000000003064 ) ) ;
#21919=ADVANCED_FACE ( 'NONE', ( #16507 ), #5762, .T. ) ;
#21928=EDGE_CURVE ( 'NONE', #19413, #21087, #19769, .T. ) ;
#21952=VERTEX_POINT ( 'NONE', #14719 ) ;
#21959=AXIS2_PLACEMENT_3D ( 'NONE', #10027, #11684, #4989 ) ;
#21968=CYLINDRICAL_SURFACE ( 'NONE', #14536, 0.3000000000000016542 ) ;
#21971=CARTESIAN_POINT ( 'NONE',  ( 30.49999999999999645, 70.00000000000000000, 10.00000000000000178 ) ) ;
#21985=DIRECTION ( 'NONE',  ( 1.000000000000000000, -0.000000000000000000, -0.000000000000000000 ) ) ;
#21998=CARTESIAN_POINT ( 'NONE',  ( 30.79999999999999716, -85.00000000000000000, 1.500000000000003997 ) ) ;
#22004=DIRECTION ( 'NONE',  ( 0.000000000000000000, 0.000000000000000000, -1.000000000000000000 ) ) ;
#22011=CYLINDRICAL_SURFACE ( 'NONE', #9546, 0.2999999999999999334 ) ;
#22033=VERTEX_POINT ( 'NONE', #12205 ) ;
#22056=FACE_OUTER_BOUND ( 'NONE', #9037, .T. ) ;
#22062=CARTESIAN_POINT ( 'NONE',  ( -30.79999999999999361, -85.00000000000000000, 1.200000000000000622 ) ) ;
#22068=ORIENTED_EDGE ( 'NONE', *, *, #19465, .T. ) ;
#22071=CIRCLE ( 'NONE', #14888, 0.3000000000000016542 ) ;
#22090=CARTESIAN_POINT ( 'NONE',  ( -34.70000000000000284, -84.70000000000001705, 0.6000000000000033085 ) ) ;
#22120=DIRECTION ( 'NONE',  ( 1.000000000000000000, 0.000000000000000000, 0.000000000000000000 ) ) ;
#22122=TOROIDAL_SURFACE ( 'NONE', #5692, 0.2999999999999999889, 0.2999999999999999889 ) ;
#22134=DIRECTION ( 'NONE',  ( 0.000000000000000000, -1.000000000000000000, 0.000000000000000000 ) ) ;
#22139=SPHERICAL_SURFACE ( 'NONE', #8158, 0.2999999999999999889 ) ;
#22140=CARTESIAN_POINT ( 'NONE',  ( 30.19999999999999574, 69.70000000000000284, 10.00000000000000178 ) ) ;
#22141=AXIS2_PLACEMENT_3D ( 'NONE', #17201, #8715, #15512 ) ;
ENDSEC;
END-ISO-10303-21;
